ISO-10303-21;
HEADER;
FILE_DESCRIPTION (('STEP AP214'),
    '1' );
FILE_NAME ('Servo-Head.step',
    '2026-11-01T06:29:40',
    ( '' ),
    ( '' ),
    'SwSTEP 2.0',
    'SolidWorks 2024',
    '' );
FILE_SCHEMA (( 'AUTOMOTIVE_DESIGN' ));
ENDSEC;

DATA;
#2=VECTOR ( 'NONE', #10690, 1000.000000000000000 ) ;
#3=CARTESIAN_POINT ( 'NONE',  ( 26.00000000000000000, 19.00000000000000000, 40.00000000000001421 ) ) ;
#15=VECTOR ( 'NONE', #3910, 1000.000000000000000 ) ;
#28=CARTESIAN_POINT ( 'NONE',  ( -20.99999999999999645, 19.00000000000000000, -35.00000000000000711 ) ) ;
#53=VERTEX_POINT ( 'NONE', #1936 ) ;
#56=DIRECTION ( 'NONE',  ( 1.000000000000000000, 0.000000000000000000, 0.000000000000000000 ) ) ;
#85=EDGE_CURVE ( 'NONE', #13473, #6022, #2032, .T. ) ;
#86=EDGE_LOOP ( 'NONE', ( #9308, #6599, #8630, #2907 ) ) ;
#87=ORIENTED_EDGE ( 'NONE', *, *, #10548, .T. ) ;
#106=VECTOR ( 'NONE', #515, 1000.000000000000000 ) ;
#122=CIRCLE ( 'NONE', #10382, 4.999999999999997335 ) ;
#132=SHAPE_DEFINITION_REPRESENTATION ( #9089, #16597 ) ;
#146=ORIENTED_EDGE ( 'NONE', *, *, #12401, .F. ) ;
#158=PRODUCT_DEFINITION ( 'UNKNOWN', '', #17864, #596 ) ;
#168=DIRECTION ( 'NONE',  ( 0.000000000000000000, 1.000000000000000000, 0.000000000000000000 ) ) ;
#169=FACE_OUTER_BOUND ( 'NONE', #20181, .T. ) ;
#173=EDGE_CURVE ( 'NONE', #9315, #975, #7926, .T. ) ;
#183=VERTEX_POINT ( 'NONE', #9617 ) ;
#212=LINE ( 'NONE', #17217, #9303 ) ;
#236=DIRECTION ( 'NONE',  ( 0.000000000000000000, -0.000000000000000000, 1.000000000000000000 ) ) ;
#241=AXIS2_PLACEMENT_3D ( 'NONE', #9899, #12700, #11340 ) ;
#262=DIRECTION ( 'NONE',  ( 0.000000000000000000, 0.000000000000000000, -1.000000000000000000 ) ) ;
#276=ORIENTED_EDGE ( 'NONE', *, *, #9042, .F. ) ;
#281=CARTESIAN_POINT ( 'NONE',  ( 26.00000000000000000, 19.00000000000000000, 31.00000000000003197 ) ) ;
#283=FACE_BOUND ( 'NONE', #20284, .T. ) ;
#298=VERTEX_POINT ( 'NONE', #7631 ) ;
#304=DIRECTION ( 'NONE',  ( 0.000000000000000000, 0.000000000000000000, -1.000000000000000000 ) ) ;
#308=EDGE_CURVE ( 'NONE', #5039, #16269, #4244, .T. ) ;
#319=CIRCLE ( 'NONE', #2951, 4.999999999999997335 ) ;
#340=CARTESIAN_POINT ( 'NONE',  ( 26.00000000000000355, 19.00000000000000000, -31.00000000000003908 ) ) ;
#356=CARTESIAN_POINT ( 'NONE',  ( 31.81980515339464333, 11.00000000000000000, 28.51980515339463906 ) ) ;
#366=APPLICATION_CONTEXT ( 'automotive_design' ) ;
#369=LINE ( 'NONE', #19334, #12012 ) ;
#382=DIRECTION ( 'NONE',  ( 0.000000000000000000, 0.000000000000000000, -1.000000000000000000 ) ) ;
#396=CARTESIAN_POINT ( 'NONE',  ( 35.00000000000000711, 8.000000000000000000, 35.00000000000000711 ) ) ;
#399=EDGE_CURVE ( 'NONE', #5413, #3192, #12898, .T. ) ;
#412=VECTOR ( 'NONE', #1213, 1000.000000000000000 ) ;
#413=AXIS2_PLACEMENT_3D ( 'NONE', #8793, #15073, #19780 ) ;
#414=ORIENTED_EDGE ( 'NONE', *, *, #903, .F. ) ;
#420=VECTOR ( 'NONE', #14227, 1000.000000000000000 ) ;
#421=LINE ( 'NONE', #4872, #10566 ) ;
#458=VECTOR ( 'NONE', #18413, 1000.000000000000000 ) ;
#459=ORIENTED_EDGE ( 'NONE', *, *, #4153, .F. ) ;
#464=AXIS2_PLACEMENT_3D ( 'NONE', #7288, #2925, #17152 ) ;
#467=EDGE_CURVE ( 'NONE', #1495, #8580, #14633, .T. ) ;
#477=CIRCLE ( 'NONE', #18244, 3.300000000000000711 ) ;
#480=DIRECTION ( 'NONE',  ( 0.000000000000000000, 0.000000000000000000, -1.000000000000000000 ) ) ;
#485=ORIENTED_EDGE ( 'NONE', *, *, #11519, .T. ) ;
#486=VECTOR ( 'NONE', #1460, 1000.000000000000000 ) ;
#502=EDGE_CURVE ( 'NONE', #13110, #6513, #14954, .T. ) ;
#515=DIRECTION ( 'NONE',  ( -0.000000000000000000, -1.000000000000000000, -0.000000000000000000 ) ) ;
#535=DIRECTION ( 'NONE',  ( -1.000000000000000000, -0.000000000000000000, -0.000000000000000000 ) ) ;
#550=ORIENTED_EDGE ( 'NONE', *, *, #7264, .F. ) ;
#551=EDGE_LOOP ( 'NONE', ( #1473, #9474, #8309, #5277 ) ) ;
#580=LINE ( 'NONE', #19423, #7154 ) ;
#585=EDGE_CURVE ( 'NONE', #12613, #10280, #7419, .T. ) ;
#588=DIRECTION ( 'NONE',  ( 0.000000000000000000, 0.000000000000000000, -1.000000000000000000 ) ) ;
#589=PLANE ( 'NONE',  #2792 ) ;
#596=PRODUCT_DEFINITION_CONTEXT ( 'detailed design', #10521, 'design' ) ;
#602=DIRECTION ( 'NONE',  ( 0.000000000000000000, 0.000000000000000000, -1.000000000000000000 ) ) ;
#608=CARTESIAN_POINT ( 'NONE',  ( -31.00000000000000000, 11.00000000000000000, 30.99999999999999289 ) ) ;
#617=ORIENTED_EDGE ( 'NONE', *, *, #12282, .F. ) ;
#665=ORIENTED_EDGE ( 'NONE', *, *, #16444, .F. ) ;
#675=DIRECTION ( 'NONE',  ( 1.000000000000000000, 0.000000000000000000, 0.000000000000000000 ) ) ;
#687=DIRECTION ( 'NONE',  ( 0.000000000000000000, 1.000000000000000000, 0.000000000000000000 ) ) ;
#715=VERTEX_POINT ( 'NONE', #6181 ) ;
#721=PLANE ( 'NONE',  #20067 ) ;
#728=CARTESIAN_POINT ( 'NONE',  ( -34.99999999999999289, 8.000000000000000000, -35.00000000000000711 ) ) ;
#733=CARTESIAN_POINT ( 'NONE',  ( 34.99999999999997868, 8.000000000000000000, -40.00000000000000711 ) ) ;
#741=CARTESIAN_POINT ( 'NONE',  ( 35.00000000000000711, 11.00000000000000000, -35.00000000000000711 ) ) ;
#758=VERTEX_POINT ( 'NONE', #12662 ) ;
#774=VECTOR ( 'NONE', #14732, 1000.000000000000000 ) ;
#781=EDGE_CURVE ( 'NONE', #8469, #13165, #477, .T. ) ;
#795=ORIENTED_EDGE ( 'NONE', *, *, #5988, .T. ) ;
#797=ORIENTED_EDGE ( 'NONE', *, *, #3489, .F. ) ;
#803=CARTESIAN_POINT ( 'NONE',  ( -31.00000000000003197, 19.00000000000000000, -26.00000000000000355 ) ) ;
#810=CARTESIAN_POINT ( 'NONE',  ( -40.00000000000000000, 19.00000000000000000, -26.00000000000000355 ) ) ;
#820=VECTOR ( 'NONE', #10129, 1000.000000000000000 ) ;
#834=ORIENTED_EDGE ( 'NONE', *, *, #8890, .F. ) ;
#840=PLANE ( 'NONE',  #1106 ) ;
#844=ORIENTED_EDGE ( 'NONE', *, *, #781, .T. ) ;
#846=DIRECTION ( 'NONE',  ( 1.000000000000000000, 0.000000000000000000, 0.000000000000000000 ) ) ;
#855=ORIENTED_EDGE ( 'NONE', *, *, #1066, .F. ) ;
#861=ORIENTED_EDGE ( 'NONE', *, *, #4153, .T. ) ;
#874=DIRECTION ( 'NONE',  ( 0.000000000000000000, 0.000000000000000000, -1.000000000000000000 ) ) ;
#877=CARTESIAN_POINT ( 'NONE',  ( 40.00000000000000711, 8.000000000000000000, -34.99999999999997868 ) ) ;
#881=PLANE ( 'NONE',  #12337 ) ;
#903=EDGE_CURVE ( 'NONE', #6513, #13719, #369, .T. ) ;
#904=DIRECTION ( 'NONE',  ( -1.000000000000000000, 0.000000000000000000, 0.000000000000000000 ) ) ;
#914=EDGE_CURVE ( 'NONE', #10510, #4609, #14497, .T. ) ;
#924=CIRCLE ( 'NONE', #12471, 3.300000000000004263 ) ;
#942=PLANE ( 'NONE',  #2598 ) ;
#953=ORIENTED_EDGE ( 'NONE', *, *, #13467, .T. ) ;
#963=DIRECTION ( 'NONE',  ( -0.000000000000000000, -1.000000000000000000, -0.000000000000000000 ) ) ;
#972=AXIS2_PLACEMENT_3D ( 'NONE', #4841, #17486, #1715 ) ;
#974=CIRCLE ( 'NONE', #10832, 3.300000000000004263 ) ;
#975=VERTEX_POINT ( 'NONE', #7190 ) ;
#980=ORIENTED_EDGE ( 'NONE', *, *, #20075, .F. ) ;
#983=DIRECTION ( 'NONE',  ( -0.000000000000000000, -1.000000000000000000, -0.000000000000000000 ) ) ;
#1006=LINE ( 'NONE', #19380, #10401 ) ;
#1018=DIRECTION ( 'NONE',  ( 1.000000000000000000, 0.000000000000000000, 0.000000000000000000 ) ) ;
#1022=VECTOR ( 'NONE', #17706, 1000.000000000000000 ) ;
#1027=CARTESIAN_POINT ( 'NONE',  ( -34.99999999999999289, 11.00000000000000000, 35.00000000000000711 ) ) ;
#1030=CARTESIAN_POINT ( 'NONE',  ( -31.00000000000000000, 11.00000000000000000, 25.99999999999999645 ) ) ;
#1052=ORIENTED_EDGE ( 'NONE', *, *, #9885, .F. ) ;
#1064=CIRCLE ( 'NONE', #18195, 4.999999999999997335 ) ;
#1066=EDGE_CURVE ( 'NONE', #6497, #17040, #9434, .T. ) ;
#1070=EDGE_CURVE ( 'NONE', #5483, #14347, #11084, .T. ) ;
#1079=VECTOR ( 'NONE', #12004, 1000.000000000000000 ) ;
#1084=ORIENTED_EDGE ( 'NONE', *, *, #13899, .F. ) ;
#1100=DIRECTION ( 'NONE',  ( -0.000000000000000000, -1.000000000000000000, -0.000000000000000000 ) ) ;
#1102=VECTOR ( 'NONE', #14007, 1000.000000000000000 ) ;
#1106=AXIS2_PLACEMENT_3D ( 'NONE', #16736, #20301, #12584 ) ;
#1123=VECTOR ( 'NONE', #9946, 1000.000000000000000 ) ;
#1131=ORIENTED_EDGE ( 'NONE', *, *, #1411, .F. ) ;
#1154=ADVANCED_FACE ( 'NONE', ( #18993 ), #4899, .F. ) ;
#1162=EDGE_CURVE ( 'NONE', #15503, #2504, #16325, .T. ) ;
#1172=CARTESIAN_POINT ( 'NONE',  ( 2.265596578422603396E-15, 19.00100000000000122, 18.50000000000000000 ) ) ;
#1177=CARTESIAN_POINT ( 'NONE',  ( 40.00000000000000711, 0.000000000000000000, 34.99999999999997868 ) ) ;
#1195=CARTESIAN_POINT ( 'NONE',  ( -40.00000000000000000, 19.00000000000000000, -26.00000000000000355 ) ) ;
#1213=DIRECTION ( 'NONE',  ( -0.000000000000000000, -1.000000000000000000, -0.000000000000000000 ) ) ;
#1223=LINE ( 'NONE', #15501, #19542 ) ;
#1227=MANIFOLD_SOLID_BREP ( 'Boss-Extrude4', #14918 ) ;
#1239=ORIENTED_EDGE ( 'NONE', *, *, #10264, .T. ) ;
#1251=DIRECTION ( 'NONE',  ( 0.000000000000000000, 0.000000000000000000, 1.000000000000000000 ) ) ;
#1269=ORIENTED_EDGE ( 'NONE', *, *, #14536, .F. ) ;
#1275=DIRECTION ( 'NONE',  ( 1.000000000000000000, 0.000000000000000000, -0.000000000000000000 ) ) ;
#1277=EDGE_CURVE ( 'NONE', #9315, #6242, #11702, .T. ) ;
#1302=DIRECTION ( 'NONE',  ( 0.000000000000000000, 1.000000000000000000, 0.000000000000000000 ) ) ;
#1313=ORIENTED_EDGE ( 'NONE', *, *, #16220, .F. ) ;
#1340=EDGE_CURVE ( 'NONE', #298, #17762, #13741, .T. ) ;
#1346=ORIENTED_EDGE ( 'NONE', *, *, #19791, .F. ) ;
#1399=CYLINDRICAL_SURFACE ( 'NONE', #972, 4.999999999999997335 ) ;
#1411=EDGE_CURVE ( 'NONE', #13058, #6497, #18882, .T. ) ;
#1412=ORIENTED_EDGE ( 'NONE', *, *, #12401, .T. ) ;
#1416=ORIENTED_EDGE ( 'NONE', *, *, #9358, .F. ) ;
#1430=FACE_OUTER_BOUND ( 'NONE', #15415, .T. ) ;
#1435=CIRCLE ( 'NONE', #11328, 35.00000000000000711 ) ;
#1441=ORIENTED_EDGE ( 'NONE', *, *, #17967, .T. ) ;
#1445=EDGE_CURVE ( 'NONE', #13536, #3873, #6849, .T. ) ;
#1446=AXIS2_PLACEMENT_3D ( 'NONE', #3134, #13745, #20006 ) ;
#1460=DIRECTION ( 'NONE',  ( -0.000000000000000000, -1.000000000000000000, -0.000000000000000000 ) ) ;
#1462=ORIENTED_EDGE ( 'NONE', *, *, #17441, .T. ) ;
#1469=VECTOR ( 'NONE', #5943, 1000.000000000000000 ) ;
#1473=ORIENTED_EDGE ( 'NONE', *, *, #10065, .F. ) ;
#1493=EDGE_LOOP ( 'NONE', ( #17586, #17289, #5838, #3950 ) ) ;
#1495=VERTEX_POINT ( 'NONE', #8279 ) ;
#1499=DIRECTION ( 'NONE',  ( 1.000000000000000000, 0.000000000000000000, 0.000000000000000000 ) ) ;
#1515=ORIENTED_EDGE ( 'NONE', *, *, #9257, .T. ) ;
#1535=ORIENTED_EDGE ( 'NONE', *, *, #9513, .F. ) ;
#1539=ORIENTED_EDGE ( 'NONE', *, *, #2609, .F. ) ;
#1547=CARTESIAN_POINT ( 'NONE',  ( -31.00000000000000000, 19.00000000000000000, 30.99999999999999289 ) ) ;
#1555=ORIENTED_EDGE ( 'NONE', *, *, #5833, .T. ) ;
#1562=ORIENTED_EDGE ( 'NONE', *, *, #9631, .F. ) ;
#1576=DIRECTION ( 'NONE',  ( 0.000000000000000000, 0.000000000000000000, 1.000000000000000000 ) ) ;
#1577=EDGE_CURVE ( 'NONE', #8466, #183, #15268, .T. ) ;
#1578=ORIENTED_EDGE ( 'NONE', *, *, #16074, .F. ) ;
#1617=CARTESIAN_POINT ( 'NONE',  ( 0.000000000000000000, -3.000000000000000000, 0.000000000000000000 ) ) ;
#1634=VECTOR ( 'NONE', #14358, 1000.000000000000000 ) ;
#1643=CARTESIAN_POINT ( 'NONE',  ( -26.00000000000000000, 19.00000000000000000, -31.00000000000003908 ) ) ;
#1647=AXIS2_PLACEMENT_3D ( 'NONE', #8447, #687, #9981 ) ;
#1650=CARTESIAN_POINT ( 'NONE',  ( 0.000000000000000000, -3.000000000000000000, 35.00000000000000711 ) ) ;
#1686=CIRCLE ( 'NONE', #8294, 3.299999999999997158 ) ;
#1692=DIRECTION ( 'NONE',  ( 1.000000000000000000, -0.000000000000000000, 0.000000000000000000 ) ) ;
#1694=CIRCLE ( 'NONE', #15889, 35.00000000000000711 ) ;
#1710=DIRECTION ( 'NONE',  ( 0.000000000000000000, 1.000000000000000000, 0.000000000000000000 ) ) ;
#1715=DIRECTION ( 'NONE',  ( 0.000000000000000000, 0.000000000000000000, -1.000000000000000000 ) ) ;
#1755=AXIS2_PLACEMENT_3D ( 'NONE', #14572, #13064, #16441 ) ;
#1793=AXIS2_PLACEMENT_3D ( 'NONE', #4623, #17185, #3065 ) ;
#1796=FACE_OUTER_BOUND ( 'NONE', #19661, .T. ) ;
#1814=DIRECTION ( 'NONE',  ( -0.000000000000000000, -0.000000000000000000, 1.000000000000000000 ) ) ;
#1831=DIRECTION ( 'NONE',  ( 0.000000000000000000, 0.000000000000000000, -1.000000000000000000 ) ) ;
#1834=EDGE_CURVE ( 'NONE', #3873, #14347, #3530, .T. ) ;
#1840=ORIENTED_EDGE ( 'NONE', *, *, #15318, .T. ) ;
#1847=DIRECTION ( 'NONE',  ( 0.000000000000000000, 0.000000000000000000, -1.000000000000000000 ) ) ;
#1874=LINE ( 'NONE', #4993, #5993 ) ;
#1876=ORIENTED_EDGE ( 'NONE', *, *, #17051, .T. ) ;
#1880=ORIENTED_EDGE ( 'NONE', *, *, #467, .T. ) ;
#1886=DIRECTION ( 'NONE',  ( 1.000000000000000000, -0.000000000000000000, 0.000000000000000000 ) ) ;
#1902=VERTEX_POINT ( 'NONE', #7034 ) ;
#1928=ORIENTED_EDGE ( 'NONE', *, *, #19444, .F. ) ;
#1936=CARTESIAN_POINT ( 'NONE',  ( 40.00000000000000711, 11.00000000000000000, -34.99999999999997868 ) ) ;
#1942=AXIS2_PLACEMENT_3D ( 'NONE', #13206, #16203, #17408 ) ;
#1948=DIRECTION ( 'NONE',  ( 0.000000000000000000, -1.000000000000000000, 0.000000000000000000 ) ) ;
#1951=ORIENTED_EDGE ( 'NONE', *, *, #8031, .F. ) ;
#1954=PLANE ( 'NONE',  #5427 ) ;
#1957=FACE_OUTER_BOUND ( 'NONE', #12979, .T. ) ;
#1964=VERTEX_POINT ( 'NONE', #8865 ) ;
#1979=DIRECTION ( 'NONE',  ( 0.000000000000000000, 1.000000000000000000, 0.000000000000000000 ) ) ;
#1984=FILL_AREA_STYLE_COLOUR ( '', #10984 ) ;
#1999=VECTOR ( 'NONE', #10175, 1000.000000000000000 ) ;
#2021=ORIENTED_EDGE ( 'NONE', *, *, #17080, .F. ) ;
#2024=ORIENTED_EDGE ( 'NONE', *, *, #15402, .F. ) ;
#2027=EDGE_CURVE ( 'NONE', #183, #5483, #19741, .T. ) ;
#2032=LINE ( 'NONE', #14638, #106 ) ;
#2050=EDGE_LOOP ( 'NONE', ( #3191, #20110, #17646, #14843 ) ) ;
#2053=EDGE_CURVE ( 'NONE', #16598, #9315, #9648, .T. ) ;
#2077=DIRECTION ( 'NONE',  ( -3.854941057726250916E-16, 0.000000000000000000, -1.000000000000000000 ) ) ;
#2083=ORIENTED_EDGE ( 'NONE', *, *, #5096, .T. ) ;
#2088=VECTOR ( 'NONE', #6691, 1000.000000000000000 ) ;
#2102=DIRECTION ( 'NONE',  ( 0.000000000000000000, -0.000000000000000000, -1.000000000000000000 ) ) ;
#2122=DIRECTION ( 'NONE',  ( -0.000000000000000000, -1.000000000000000000, -0.000000000000000000 ) ) ;
#2132=CYLINDRICAL_SURFACE ( 'NONE', #4228, 10.00000000000000178 ) ;
#2134=FACE_BOUND ( 'NONE', #17596, .T. ) ;
#2180=CARTESIAN_POINT ( 'NONE',  ( -39.99999999999999289, 0.000000000000000000, 34.99999999999997868 ) ) ;
#2181=ORIENTED_EDGE ( 'NONE', *, *, #5155, .F. ) ;
#2186=ORIENTED_EDGE ( 'NONE', *, *, #4845, .T. ) ;
#2198=ADVANCED_FACE ( 'NONE', ( #9299 ), #13942, .T. ) ;
#2220=FACE_OUTER_BOUND ( 'NONE', #11476, .T. ) ;
#2222=CARTESIAN_POINT ( 'NONE',  ( -31.00000000000000000, 19.00000000000000000, 30.99999999999999289 ) ) ;
#2230=EDGE_LOOP ( 'NONE', ( #2624, #7326 ) ) ;
#2232=ORIENTED_EDGE ( 'NONE', *, *, #14175, .F. ) ;
#2248=CARTESIAN_POINT ( 'NONE',  ( -26.00000000000000000, 19.00000000000000000, -40.00000000000000711 ) ) ;
#2261=ADVANCED_FACE ( 'NONE', ( #1957 ), #13038, .F. ) ;
#2267=FACE_OUTER_BOUND ( 'NONE', #7036, .T. ) ;
#2268=CARTESIAN_POINT ( 'NONE',  ( -26.00000000000000355, 19.00000000000000000, 31.00000000000003197 ) ) ;
#2278=AXIS2_PLACEMENT_3D ( 'NONE', #15184, #13640, #19905 ) ;
#2289=( NAMED_UNIT ( * ) SI_UNIT ( $, .STERADIAN. ) SOLID_ANGLE_UNIT ( ) );
#2312=EDGE_CURVE ( 'NONE', #9509, #3967, #18971, .T. ) ;
#2314=EDGE_LOOP ( 'NONE', ( #5407, #10763, #2974, #1539, #14422, #16401, #5352, #4326 ) ) ;
#2368=ORIENTED_EDGE ( 'NONE', *, *, #308, .F. ) ;
#2384=DIRECTION ( 'NONE',  ( -0.000000000000000000, -1.000000000000000000, -0.000000000000000000 ) ) ;
#2385=CARTESIAN_POINT ( 'NONE',  ( 31.00000000000003553, 8.000000000000000000, 20.99999999999999289 ) ) ;
#2401=AXIS2_PLACEMENT_3D ( 'NONE', #6412, #7746, #12699 ) ;
#2416=ORIENTED_EDGE ( 'NONE', *, *, #15113, .F. ) ;
#2424=DIRECTION ( 'NONE',  ( 0.000000000000000000, 1.000000000000000000, 0.000000000000000000 ) ) ;
#2440=FACE_BOUND ( 'NONE', #7812, .T. ) ;
#2492=EDGE_CURVE ( 'NONE', #5205, #15503, #1006, .T. ) ;
#2504=VERTEX_POINT ( 'NONE', #5890 ) ;
#2505=AXIS2_PLACEMENT_3D ( 'NONE', #4417, #4316, #10595 ) ;
#2507=CARTESIAN_POINT ( 'NONE',  ( -20.99999999999999645, 19.00000000000000000, 35.00000000000001421 ) ) ;
#2549=ADVANCED_FACE ( 'NONE', ( #10826 ), #4646, .F. ) ;
#2557=AXIS2_PLACEMENT_3D ( 'NONE', #11929, #10385, #14610 ) ;
#2561=CYLINDRICAL_SURFACE ( 'NONE', #5055, 3.299999999999997158 ) ;
#2566=ADVANCED_FACE ( 'NONE', ( #12901 ), #14116, .F. ) ;
#2570=AXIS2_PLACEMENT_3D ( 'NONE', #19503, #5221, #2102 ) ;
#2575=DIRECTION ( 'NONE',  ( 0.000000000000000000, 0.000000000000000000, 1.000000000000000000 ) ) ;
#2580=EDGE_CURVE ( 'NONE', #5279, #13880, #16108, .T. ) ;
#2585=CARTESIAN_POINT ( 'NONE',  ( 34.99999999999997868, 0.000000000000000000, -40.00000000000000711 ) ) ;
#2593=CARTESIAN_POINT ( 'NONE',  ( -26.00000000000000000, 11.00000000000000000, 40.00000000000000711 ) ) ;
#2595=ORIENTED_EDGE ( 'NONE', *, *, #19556, .T. ) ;
#2598=AXIS2_PLACEMENT_3D ( 'NONE', #18469, #9002, #4363 ) ;
#2601=FACE_OUTER_BOUND ( 'NONE', #10394, .T. ) ;
#2608=EDGE_CURVE ( 'NONE', #7143, #6864, #14428, .T. ) ;
#2609=EDGE_CURVE ( 'NONE', #9862, #14625, #3300, .T. ) ;
#2624=ORIENTED_EDGE ( 'NONE', *, *, #9358, .T. ) ;
#2649=ORIENTED_EDGE ( 'NONE', *, *, #9103, .T. ) ;
#2653=ORIENTED_EDGE ( 'NONE', *, *, #9894, .T. ) ;
#2658=CARTESIAN_POINT ( 'NONE',  ( -34.99999999999996447, 0.000000000000000000, 40.00000000000000711 ) ) ;
#2666=DIRECTION ( 'NONE',  ( 0.000000000000000000, -1.000000000000000000, 0.000000000000000000 ) ) ;
#2669=CARTESIAN_POINT ( 'NONE',  ( -26.00000000000000000, 11.00000000000000000, 40.00000000000000711 ) ) ;
#2670=ADVANCED_FACE ( 'NONE', ( #17322 ), #14525, .F. ) ;
#2672=ORIENTED_EDGE ( 'NONE', *, *, #17630, .T. ) ;
#2683=ADVANCED_FACE ( 'NONE', ( #15786 ), #6503, .T. ) ;
#2685=AXIS2_PLACEMENT_3D ( 'NONE', #9853, #6789, #14705 ) ;
#2713=ORIENTED_EDGE ( 'NONE', *, *, #18956, .T. ) ;
#2741=AXIS2_PLACEMENT_3D ( 'NONE', #5042, #3500, #8234 ) ;
#2743=PLANE ( 'NONE',  #5032 ) ;
#2747=CARTESIAN_POINT ( 'NONE',  ( -31.00000000000003553, 19.00000000000000000, -21.00000000000000000 ) ) ;
#2750=ORIENTED_EDGE ( 'NONE', *, *, #5322, .T. ) ;
#2751=AXIS2_PLACEMENT_3D ( 'NONE', #18914, #10991, #262 ) ;
#2778=ORIENTED_EDGE ( 'NONE', *, *, #1445, .T. ) ;
#2780=LINE ( 'NONE', #15476, #6810 ) ;
#2789=DIRECTION ( 'NONE',  ( -0.000000000000000000, -1.000000000000000000, -0.000000000000000000 ) ) ;
#2792=AXIS2_PLACEMENT_3D ( 'NONE', #8337, #8139, #6590 ) ;
#2806=DIRECTION ( 'NONE',  ( 0.000000000000000000, 0.000000000000000000, 1.000000000000000000 ) ) ;
#2822=EDGE_LOOP ( 'NONE', ( #4254, #17363, #6472, #2021, #9117, #3380, #13904, #16146, #10816, #12588, #7786, #2952, #2232, #18985, #15182, #797 ) ) ;
#2853=PLANE ( 'NONE',  #16692 ) ;
#2854=EDGE_LOOP ( 'NONE', ( #16353, #18066, #6274, #4703 ) ) ;
#2869=DIRECTION ( 'NONE',  ( 0.000000000000000000, 0.000000000000000000, -1.000000000000000000 ) ) ;
#2875=EDGE_LOOP ( 'NONE', ( #10252, #12287, #87, #18860, #4916, #8454 ) ) ;
#2881=AXIS2_PLACEMENT_3D ( 'NONE', #17704, #9460, #3280 ) ;
#2896=ORIENTED_EDGE ( 'NONE', *, *, #16318, .T. ) ;
#2907=ORIENTED_EDGE ( 'NONE', *, *, #1577, .T. ) ;
#2918=AXIS2_PLACEMENT_3D ( 'NONE', #15600, #19344, #15490 ) ;
#2923=ORIENTED_EDGE ( 'NONE', *, *, #7535, .T. ) ;
#2925=DIRECTION ( 'NONE',  ( -1.000000000000000000, 0.000000000000000000, 0.000000000000000000 ) ) ;
#2947=EDGE_CURVE ( 'NONE', #3192, #17522, #14703, .T. ) ;
#2951=AXIS2_PLACEMENT_3D ( 'NONE', #14995, #7556, #16943 ) ;
#2952=ORIENTED_EDGE ( 'NONE', *, *, #2053, .F. ) ;
#2968=DIRECTION ( 'NONE',  ( 0.000000000000000000, 0.000000000000000000, 1.000000000000000000 ) ) ;
#2974=ORIENTED_EDGE ( 'NONE', *, *, #9373, .F. ) ;
#2986=DIRECTION ( 'NONE',  ( -0.000000000000000000, -1.000000000000000000, -0.000000000000000000 ) ) ;
#3005=ORIENTED_EDGE ( 'NONE', *, *, #17121, .F. ) ;
#3007=DIRECTION ( 'NONE',  ( -0.000000000000000000, -1.000000000000000000, -0.000000000000000000 ) ) ;
#3012=CARTESIAN_POINT ( 'NONE',  ( 31.00000000000003908, 19.00000000000000000, -26.00000000000000355 ) ) ;
#3018=ORIENTED_EDGE ( 'NONE', *, *, #11519, .F. ) ;
#3028=ORIENTED_EDGE ( 'NONE', *, *, #5988, .F. ) ;
#3034=DIRECTION ( 'NONE',  ( -0.000000000000000000, -1.000000000000000000, -0.000000000000000000 ) ) ;
#3042=DIRECTION ( 'NONE',  ( -0.000000000000000000, -1.000000000000000000, -0.000000000000000000 ) ) ;
#3047=VECTOR ( 'NONE', #7244, 1000.000000000000000 ) ;
#3065=DIRECTION ( 'NONE',  ( 0.000000000000000000, 0.000000000000000000, 1.000000000000000000 ) ) ;
#3071=DIRECTION ( 'NONE',  ( -0.000000000000000000, -1.000000000000000000, -0.000000000000000000 ) ) ;
#3079=( GEOMETRIC_REPRESENTATION_CONTEXT ( 3 ) GLOBAL_UNCERTAINTY_ASSIGNED_CONTEXT ( ( #14877 ) ) GLOBAL_UNIT_ASSIGNED_CONTEXT ( ( #14476, #5215, #2289 ) ) REPRESENTATION_CONTEXT ( 'NONE', 'WORKASPACE' ) );
#3127=CIRCLE ( 'NONE', #14992, 18.50000000000000000 ) ;
#3130=ADVANCED_FACE ( 'NONE', ( #2220 ), #15020, .F. ) ;
#3134=CARTESIAN_POINT ( 'NONE',  ( 31.00000000000000000, 19.00000000000000000, -31.00000000000000355 ) ) ;
#3153=EDGE_LOOP ( 'NONE', ( #1346, #11323, #9713, #9987 ) ) ;
#3190=ADVANCED_FACE ( 'NONE', ( #14807 ), #7101, .F. ) ;
#3191=ORIENTED_EDGE ( 'NONE', *, *, #1162, .F. ) ;
#3192=VERTEX_POINT ( 'NONE', #16576 ) ;
#3198=CARTESIAN_POINT ( 'NONE',  ( -39.99999999999999289, 11.00000000000000000, -34.99999999999997868 ) ) ;
#3203=DIRECTION ( 'NONE',  ( 0.000000000000000000, 0.000000000000000000, -1.000000000000000000 ) ) ;
#3211=EDGE_CURVE ( 'NONE', #1495, #11244, #1694, .T. ) ;
#3223=DIRECTION ( 'NONE',  ( 1.000000000000000000, -0.000000000000000000, 0.000000000000000000 ) ) ;
#3228=DIRECTION ( 'NONE',  ( -0.000000000000000000, -1.000000000000000000, -0.000000000000000000 ) ) ;
#3230=ORIENTED_EDGE ( 'NONE', *, *, #20156, .T. ) ;
#3251=DIRECTION ( 'NONE',  ( 0.000000000000000000, 0.000000000000000000, -1.000000000000000000 ) ) ;
#3260=DIRECTION ( 'NONE',  ( 0.000000000000000000, -1.000000000000000000, 0.000000000000000000 ) ) ;
#3280=DIRECTION ( 'NONE',  ( 0.000000000000000000, 0.000000000000000000, -1.000000000000000000 ) ) ;
#3289=EDGE_LOOP ( 'NONE', ( #8007, #17385, #10800, #13124 ) ) ;
#3294=ORIENTED_EDGE ( 'NONE', *, *, #18304, .T. ) ;
#3295=FACE_OUTER_BOUND ( 'NONE', #4028, .T. ) ;
#3300=LINE ( 'NONE', #17409, #5804 ) ;
#3334=ADVANCED_FACE ( 'NONE', ( #9747 ), #12529, .F. ) ;
#3341=EDGE_LOOP ( 'NONE', ( #9241, #1562, #8666, #9673 ) ) ;
#3343=CARTESIAN_POINT ( 'NONE',  ( 26.00000000000000000, 19.00000000000000000, -40.00000000000000711 ) ) ;
#3363=FACE_OUTER_BOUND ( 'NONE', #7853, .T. ) ;
#3380=ORIENTED_EDGE ( 'NONE', *, *, #1445, .F. ) ;
#3384=CARTESIAN_POINT ( 'NONE',  ( -20.99999999999999645, 19.00000000000000000, 35.00000000000001421 ) ) ;
#3410=ORIENTED_EDGE ( 'NONE', *, *, #9631, .T. ) ;
#3415=EDGE_CURVE ( 'NONE', #758, #12917, #9630, .T. ) ;
#3418=VECTOR ( 'NONE', #12248, 1000.000000000000000 ) ;
#3438=DIRECTION ( 'NONE',  ( -0.000000000000000000, -1.000000000000000000, -0.000000000000000000 ) ) ;
#3449=ORIENTED_EDGE ( 'NONE', *, *, #2580, .F. ) ;
#3482=VERTEX_POINT ( 'NONE', #3566 ) ;
#3488=ORIENTED_EDGE ( 'NONE', *, *, #502, .F. ) ;
#3489=EDGE_CURVE ( 'NONE', #17522, #16867, #14578, .T. ) ;
#3500=DIRECTION ( 'NONE',  ( 0.000000000000000000, 0.000000000000000000, 1.000000000000000000 ) ) ;
#3519=DIRECTION ( 'NONE',  ( -0.000000000000000000, -0.000000000000000000, 1.000000000000000000 ) ) ;
#3530=LINE ( 'NONE', #19172, #15659 ) ;
#3538=ORIENTED_EDGE ( 'NONE', *, *, #8692, .F. ) ;
#3550=CIRCLE ( 'NONE', #241, 18.50000000000000000 ) ;
#3553=ORIENTED_EDGE ( 'NONE', *, *, #20294, .F. ) ;
#3566=CARTESIAN_POINT ( 'NONE',  ( -35.00000000000000000, 8.000000000000000000, 20.99999999999999289 ) ) ;
#3584=ORIENTED_EDGE ( 'NONE', *, *, #18299, .T. ) ;
#3601=CYLINDRICAL_SURFACE ( 'NONE', #15451, 4.999999999999997335 ) ;
#3605=EDGE_CURVE ( 'NONE', #18105, #20055, #15702, .T. ) ;
#3610=VERTEX_POINT ( 'NONE', #12172 ) ;
#3612=CARTESIAN_POINT ( 'NONE',  ( -34.99999999999999289, 0.000000000000000000, 35.00000000000000711 ) ) ;
#3628=VERTEX_POINT ( 'NONE', #15485 ) ;
#3653=EDGE_LOOP ( 'NONE', ( #16572, #10093, #1441, #12892 ) ) ;
#3695=LINE ( 'NONE', #14812, #1022 ) ;
#3714=EDGE_CURVE ( 'NONE', #4513, #6680, #3550, .T. ) ;
#3733=ORIENTED_EDGE ( 'NONE', *, *, #173, .T. ) ;
#3746=ORIENTED_EDGE ( 'NONE', *, *, #903, .T. ) ;
#3767=DIRECTION ( 'NONE',  ( 0.000000000000000000, 0.000000000000000000, -1.000000000000000000 ) ) ;
#3851=CARTESIAN_POINT ( 'NONE',  ( 26.00000000000000000, 11.00000000000000000, 31.00000000000003197 ) ) ;
#3863=CYLINDRICAL_SURFACE ( 'NONE', #14149, 3.299999999999997158 ) ;
#3873=VERTEX_POINT ( 'NONE', #14740 ) ;
#3878=LINE ( 'NONE', #11498, #9937 ) ;
#3881=EDGE_CURVE ( 'NONE', #12403, #5525, #16730, .T. ) ;
#3893=DIRECTION ( 'NONE',  ( -1.000000000000000000, 0.000000000000000000, -0.000000000000000000 ) ) ;
#3910=DIRECTION ( 'NONE',  ( -0.000000000000000000, -1.000000000000000000, -0.000000000000000000 ) ) ;
#3942=ORIENTED_EDGE ( 'NONE', *, *, #12512, .T. ) ;
#3943=DIRECTION ( 'NONE',  ( 0.000000000000000000, 0.000000000000000000, 1.000000000000000000 ) ) ;
#3949=CIRCLE ( 'NONE', #15484, 3.299999999999997158 ) ;
#3950=ORIENTED_EDGE ( 'NONE', *, *, #11254, .T. ) ;
#3967=VERTEX_POINT ( 'NONE', #13503 ) ;
#3979=VERTEX_POINT ( 'NONE', #15458 ) ;
#3982=ORIENTED_EDGE ( 'NONE', *, *, #17986, .T. ) ;
#3996=CARTESIAN_POINT ( 'NONE',  ( -20.99999999999999645, 19.00000000000000000, -35.00000000000000711 ) ) ;
#3998=CARTESIAN_POINT ( 'NONE',  ( 31.00000000000000000, 11.00000000000000000, 30.99999999999999289 ) ) ;
#3999=DIRECTION ( 'NONE',  ( -1.000000000000000000, 0.000000000000000000, 0.000000000000000000 ) ) ;
#4001=CARTESIAN_POINT ( 'NONE',  ( 35.00000000000000711, 8.000000000000000000, 20.99999999999999289 ) ) ;
#4028=EDGE_LOOP ( 'NONE', ( #18653, #1880, #861, #19417 ) ) ;
#4050=CIRCLE ( 'NONE', #17523, 35.00000000000000711 ) ;
#4077=ORIENTED_EDGE ( 'NONE', *, *, #5833, .F. ) ;
#4083=ORIENTED_EDGE ( 'NONE', *, *, #9103, .F. ) ;
#4089=ORIENTED_EDGE ( 'NONE', *, *, #15477, .T. ) ;
#4099=EDGE_CURVE ( 'NONE', #3482, #1964, #12672, .T. ) ;
#4104=CARTESIAN_POINT ( 'NONE',  ( -31.00000000000000000, 11.00000000000000000, 30.99999999999999289 ) ) ;
#4147=ORIENTED_EDGE ( 'NONE', *, *, #16565, .T. ) ;
#4153=EDGE_CURVE ( 'NONE', #8580, #3628, #13125, .T. ) ;
#4157=DIRECTION ( 'NONE',  ( 0.000000000000000000, 0.000000000000000000, 1.000000000000000000 ) ) ;
#4159=PLANE ( 'NONE',  #8986 ) ;
#4220=EDGE_CURVE ( 'NONE', #6120, #715, #19983, .T. ) ;
#4228=AXIS2_PLACEMENT_3D ( 'NONE', #2222, #17798, #588 ) ;
#4232=FACE_OUTER_BOUND ( 'NONE', #16219, .T. ) ;
#4242=ORIENTED_EDGE ( 'NONE', *, *, #3881, .F. ) ;
#4244=LINE ( 'NONE', #18441, #16280 ) ;
#4254=ORIENTED_EDGE ( 'NONE', *, *, #2947, .F. ) ;
#4284=DIRECTION ( 'NONE',  ( -0.000000000000000000, -1.000000000000000000, -0.000000000000000000 ) ) ;
#4285=VERTEX_POINT ( 'NONE', #5341 ) ;
#4298=DIRECTION ( 'NONE',  ( -0.000000000000000000, -1.000000000000000000, -0.000000000000000000 ) ) ;
#4310=ORIENTED_EDGE ( 'NONE', *, *, #18299, .F. ) ;
#4316=DIRECTION ( 'NONE',  ( -0.000000000000000000, -1.000000000000000000, 0.000000000000000000 ) ) ;
#4322=FACE_OUTER_BOUND ( 'NONE', #10260, .T. ) ;
#4323=ADVANCED_FACE ( 'NONE', ( #15024 ), #2132, .T. ) ;
#4326=ORIENTED_EDGE ( 'NONE', *, *, #7264, .T. ) ;
#4333=ORIENTED_EDGE ( 'NONE', *, *, #3714, .T. ) ;
#4340=DIRECTION ( 'NONE',  ( -1.000000000000000000, 0.000000000000000000, -0.000000000000000000 ) ) ;
#4342=CARTESIAN_POINT ( 'NONE',  ( -31.00000000000003553, 19.00000000000000000, -21.00000000000000000 ) ) ;
#4344=CIRCLE ( 'NONE', #2685, 4.999999999999997335 ) ;
#4363=DIRECTION ( 'NONE',  ( -1.000000000000000000, 0.000000000000000000, -0.000000000000000000 ) ) ;
#4379=EDGE_CURVE ( 'NONE', #6860, #5413, #6050, .T. ) ;
#4392=LINE ( 'NONE', #5746, #18357 ) ;
#4400=ORIENTED_EDGE ( 'NONE', *, *, #3489, .T. ) ;
#4404=EDGE_LOOP ( 'NONE', ( #11295, #7039, #1416, #7783 ) ) ;
#4415=VECTOR ( 'NONE', #17545, 1000.000000000000000 ) ;
#4417=CARTESIAN_POINT ( 'NONE',  ( -31.00000000000000000, 19.00000000000000000, -31.00000000000000000 ) ) ;
#4419=VECTOR ( 'NONE', #2384, 1000.000000000000000 ) ;
#4442=VECTOR ( 'NONE', #2122, 1000.000000000000000 ) ;
#4458=VECTOR ( 'NONE', #12815, 1000.000000000000000 ) ;
#4468=DIRECTION ( 'NONE',  ( 0.000000000000000000, 0.000000000000000000, -1.000000000000000000 ) ) ;
#4486=EDGE_CURVE ( 'NONE', #13473, #8466, #4392, .T. ) ;
#4506=AXIS2_PLACEMENT_3D ( 'NONE', #11822, #2424, #6890 ) ;
#4511=DIRECTION ( 'NONE',  ( 0.000000000000000000, 0.000000000000000000, 1.000000000000000000 ) ) ;
#4513=VERTEX_POINT ( 'NONE', #13869 ) ;
#4530=CARTESIAN_POINT ( 'NONE',  ( 31.00000000000000000, 19.00000000000000000, 30.99999999999999289 ) ) ;
#4545=LINE ( 'NONE', #18243, #4984 ) ;
#4609=VERTEX_POINT ( 'NONE', #6462 ) ;
#4618=DIRECTION ( 'NONE',  ( 0.000000000000000000, 0.000000000000000000, 1.000000000000000000 ) ) ;
#4623=CARTESIAN_POINT ( 'NONE',  ( 31.00000000000000000, 11.00000000000000000, -31.00000000000000355 ) ) ;
#4627=CARTESIAN_POINT ( 'NONE',  ( -20.99999999999999645, 19.00000000000000000, 31.00000000000003197 ) ) ;
#4635=ORIENTED_EDGE ( 'NONE', *, *, #20156, .F. ) ;
#4646=CYLINDRICAL_SURFACE ( 'NONE', #8759, 4.999999999999997335 ) ;
#4660=ORIENTED_EDGE ( 'NONE', *, *, #8031, .T. ) ;
#4666=AXIS2_PLACEMENT_3D ( 'NONE', #17175, #17383, #11004 ) ;
#4673=CARTESIAN_POINT ( 'NONE',  ( -39.99999999999999289, 8.000000000000000000, 34.99999999999997868 ) ) ;
#4676=VERTEX_POINT ( 'NONE', #10245 ) ;
#4682=LINE ( 'NONE', #3343, #16974 ) ;
#4685=ORIENTED_EDGE ( 'NONE', *, *, #18355, .F. ) ;
#4689=CYLINDRICAL_SURFACE ( 'NONE', #7888, 35.00000000000000711 ) ;
#4703=ORIENTED_EDGE ( 'NONE', *, *, #12904, .T. ) ;
#4711=AXIS2_PLACEMENT_3D ( 'NONE', #18963, #11136, #7751 ) ;
#4736=ADVANCED_FACE ( 'NONE', ( #5423, #19319 ), #16263, .F. ) ;
#4738=DIRECTION ( 'NONE',  ( -0.000000000000000000, -1.000000000000000000, -0.000000000000000000 ) ) ;
#4780=DIRECTION ( 'NONE',  ( 0.000000000000000000, 0.000000000000000000, -1.000000000000000000 ) ) ;
#4782=DIRECTION ( 'NONE',  ( 1.000000000000000000, 0.000000000000000000, 0.000000000000000000 ) ) ;
#4818=CARTESIAN_POINT ( 'NONE',  ( -39.99999999999999289, 0.000000000000000000, -34.99999999999997868 ) ) ;
#4819=CARTESIAN_POINT ( 'NONE',  ( 35.00000000000000711, 19.00000000000000000, -21.00000000000000355 ) ) ;
#4841=CARTESIAN_POINT ( 'NONE',  ( -31.00000000000000000, 19.00000000000000000, 30.99999999999999289 ) ) ;
#4845=EDGE_CURVE ( 'NONE', #19815, #18235, #18380, .T. ) ;
#4872=CARTESIAN_POINT ( 'NONE',  ( -39.99999999999999289, 0.000000000000000000, 34.99999999999997868 ) ) ;
#4873=ORIENTED_EDGE ( 'NONE', *, *, #2608, .F. ) ;
#4892=CARTESIAN_POINT ( 'NONE',  ( 40.00000000000000711, 8.000000000000000000, 34.99999999999997868 ) ) ;
#4898=ORIENTED_EDGE ( 'NONE', *, *, #3605, .T. ) ;
#4899=CYLINDRICAL_SURFACE ( 'NONE', #15605, 5.000000000000000888 ) ;
#4916=ORIENTED_EDGE ( 'NONE', *, *, #5231, .T. ) ;
#4936=CARTESIAN_POINT ( 'NONE',  ( 26.00000000000000000, 19.00000000000000000, 40.00000000000001421 ) ) ;
#4961=ADVANCED_FACE ( 'NONE', ( #17348, #8083 ), #9417, .T. ) ;
#4964=DIRECTION ( 'NONE',  ( 0.000000000000000000, 0.000000000000000000, -1.000000000000000000 ) ) ;
#4976=CARTESIAN_POINT ( 'NONE',  ( -20.99999999999999645, 8.000000000000000000, -35.00000000000000711 ) ) ;
#4984=VECTOR ( 'NONE', #11974, 1000.000000000000000 ) ;
#4990=DIRECTION ( 'NONE',  ( 0.000000000000000000, 0.000000000000000000, 1.000000000000000000 ) ) ;
#4993=CARTESIAN_POINT ( 'NONE',  ( 0.000000000000000000, -3.000000000000000000, 35.00000000000000711 ) ) ;
#4994=VERTEX_POINT ( 'NONE', #9727 ) ;
#5013=ORIENTED_EDGE ( 'NONE', *, *, #15577, .T. ) ;
#5031=CARTESIAN_POINT ( 'NONE',  ( 31.81980515339464333, 11.00000000000000000, 35.11980515339463693 ) ) ;
#5032=AXIS2_PLACEMENT_3D ( 'NONE', #10476, #13395, #16984 ) ;
#5039=VERTEX_POINT ( 'NONE', #8026 ) ;
#5042=CARTESIAN_POINT ( 'NONE',  ( 0.000000000000000000, 0.000000000000000000, 0.000000000000000000 ) ) ;
#5055=AXIS2_PLACEMENT_3D ( 'NONE', #9557, #3071, #11113 ) ;
#5096=EDGE_CURVE ( 'NONE', #14619, #19590, #924, .T. ) ;
#5135=AXIS2_PLACEMENT_3D ( 'NONE', #6253, #12530, #18794 ) ;
#5137=DIRECTION ( 'NONE',  ( -0.000000000000000000, -0.000000000000000000, 1.000000000000000000 ) ) ;
#5141=VERTEX_POINT ( 'NONE', #10438 ) ;
#5143=ORIENTED_EDGE ( 'NONE', *, *, #13900, .F. ) ;
#5155=EDGE_CURVE ( 'NONE', #758, #4994, #17749, .T. ) ;
#5169=DIRECTION ( 'NONE',  ( 0.000000000000000000, 1.000000000000000000, -0.000000000000000000 ) ) ;
#5181=LINE ( 'NONE', #2248, #8699 ) ;
#5190=CARTESIAN_POINT ( 'NONE',  ( 40.00000000000000711, 19.00000000000000000, 25.99999999999999645 ) ) ;
#5205=VERTEX_POINT ( 'NONE', #8339 ) ;
#5208=ORIENTED_EDGE ( 'NONE', *, *, #18040, .F. ) ;
#5215=( NAMED_UNIT ( * ) PLANE_ANGLE_UNIT ( ) SI_UNIT ( $, .RADIAN. ) );
#5221=DIRECTION ( 'NONE',  ( 0.000000000000000000, -1.000000000000000000, 0.000000000000000000 ) ) ;
#5231=EDGE_CURVE ( 'NONE', #12661, #16049, #18663, .T. ) ;
#5232=EDGE_LOOP ( 'NONE', ( #4898, #3553, #4873, #11660 ) ) ;
#5238=VERTEX_POINT ( 'NONE', #12779 ) ;
#5242=ADVANCED_FACE ( 'NONE', ( #11428 ), #3601, .T. ) ;
#5251=ORIENTED_EDGE ( 'NONE', *, *, #17441, .F. ) ;
#5255=ORIENTED_EDGE ( 'NONE', *, *, #5949, .T. ) ;
#5276=EDGE_CURVE ( 'NONE', #15939, #12917, #16777, .T. ) ;
#5277=ORIENTED_EDGE ( 'NONE', *, *, #16074, .T. ) ;
#5279=VERTEX_POINT ( 'NONE', #4936 ) ;
#5310=VECTOR ( 'NONE', #2869, 1000.000000000000000 ) ;
#5321=CARTESIAN_POINT ( 'NONE',  ( -34.99999999999996447, 8.000000000000000000, -40.00000000000000711 ) ) ;
#5322=EDGE_CURVE ( 'NONE', #12613, #9677, #10507, .T. ) ;
#5332=DIRECTION ( 'NONE',  ( 0.000000000000000000, 0.000000000000000000, -1.000000000000000000 ) ) ;
#5341=CARTESIAN_POINT ( 'NONE',  ( -31.81980515339462912, 0.000000000000000000, -35.11980515339465114 ) ) ;
#5342=( LENGTH_UNIT ( ) NAMED_UNIT ( * ) SI_UNIT ( .MILLI., .METRE. ) );
#5343=FACE_BOUND ( 'NONE', #2230, .T. ) ;
#5347=CARTESIAN_POINT ( 'NONE',  ( -26.00000000000000000, 19.00000000000000000, 40.00000000000001421 ) ) ;
#5352=ORIENTED_EDGE ( 'NONE', *, *, #7113, .T. ) ;
#5364=FACE_OUTER_BOUND ( 'NONE', #2050, .T. ) ;
#5368=DIRECTION ( 'NONE',  ( 0.000000000000000000, 1.000000000000000000, 0.000000000000000000 ) ) ;
#5399=LINE ( 'NONE', #733, #4419 ) ;
#5407=ORIENTED_EDGE ( 'NONE', *, *, #15220, .F. ) ;
#5413=VERTEX_POINT ( 'NONE', #3996 ) ;
#5416=FACE_OUTER_BOUND ( 'NONE', #15128, .T. ) ;
#5423=FACE_OUTER_BOUND ( 'NONE', #8238, .T. ) ;
#5427=AXIS2_PLACEMENT_3D ( 'NONE', #14751, #8273, #14545 ) ;
#5444=DIRECTION ( 'NONE',  ( 0.000000000000000000, -1.000000000000000000, 0.000000000000000000 ) ) ;
#5468=CIRCLE ( 'NONE', #18951, 3.299999999999997158 ) ;
#5483=VERTEX_POINT ( 'NONE', #8930 ) ;
#5493=CIRCLE ( 'NONE', #4506, 3.299999999999997158 ) ;
#5508=FACE_OUTER_BOUND ( 'NONE', #12392, .T. ) ;
#5525=VERTEX_POINT ( 'NONE', #1030 ) ;
#5551=EDGE_LOOP ( 'NONE', ( #11870, #15014, #1951, #1535 ) ) ;
#5566=CARTESIAN_POINT ( 'NONE',  ( -31.81980515339462912, 0.000000000000000000, 28.51980515339464972 ) ) ;
#5571=VERTEX_POINT ( 'NONE', #11899 ) ;
#5606=VECTOR ( 'NONE', #19758, 1000.000000000000000 ) ;
#5624=ORIENTED_EDGE ( 'NONE', *, *, #2609, .T. ) ;
#5649=ORIENTED_EDGE ( 'NONE', *, *, #18040, .T. ) ;
#5662=DIRECTION ( 'NONE',  ( 0.000000000000000000, -0.000000000000000000, -1.000000000000000000 ) ) ;
#5669=ORIENTED_EDGE ( 'NONE', *, *, #1834, .F. ) ;
#5682=CARTESIAN_POINT ( 'NONE',  ( 35.00000000000000711, 19.00000000000000000, 20.99999999999999289 ) ) ;
#5689=VECTOR ( 'NONE', #14269, 1000.000000000000000 ) ;
#5693=DIRECTION ( 'NONE',  ( -1.000000000000000000, 0.000000000000000000, 0.000000000000000000 ) ) ;
#5708=CIRCLE ( 'NONE', #2401, 4.999999999999997335 ) ;
#5720=ORIENTED_EDGE ( 'NONE', *, *, #14282, .T. ) ;
#5746=CARTESIAN_POINT ( 'NONE',  ( 31.00000000000003553, 19.00000000000000000, 20.99999999999999289 ) ) ;
#5775=CARTESIAN_POINT ( 'NONE',  ( -26.00000000000000355, 19.00000000000000000, 31.00000000000003197 ) ) ;
#5780=MECHANICAL_DESIGN_GEOMETRIC_PRESENTATION_REPRESENTATION('',(#18919),#3079);
#5787=ADVANCED_FACE ( 'NONE', ( #17971 ), #3863, .F. ) ;
#5790=AXIS2_PLACEMENT_3D ( 'NONE', #15396, #4468, #15612 ) ;
#5804=VECTOR ( 'NONE', #3519, 1000.000000000000000 ) ;
#5816=LINE ( 'NONE', #9711, #10358 ) ;
#5833=EDGE_CURVE ( 'NONE', #13589, #8514, #319, .T. ) ;
#5838=ORIENTED_EDGE ( 'NONE', *, *, #4379, .T. ) ;
#5845=CARTESIAN_POINT ( 'NONE',  ( -31.00000000000003553, 11.00000000000000000, -26.00000000000000355 ) ) ;
#5853=DIRECTION ( 'NONE',  ( 0.000000000000000000, 1.000000000000000000, 0.000000000000000000 ) ) ;
#5854=CARTESIAN_POINT ( 'NONE',  ( 31.00000000000003553, 19.00000000000000000, 20.99999999999999289 ) ) ;
#5878=EDGE_CURVE ( 'NONE', #5238, #12661, #18754, .T. ) ;
#5880=CARTESIAN_POINT ( 'NONE',  ( 31.00000000000000000, 8.000000000000000000, 30.99999999999999289 ) ) ;
#5884=AXIS2_PLACEMENT_3D ( 'NONE', #7778, #12507, #236 ) ;
#5889=CARTESIAN_POINT ( 'NONE',  ( 21.00000000000000000, 19.00000000000000000, 35.00000000000001421 ) ) ;
#5890=CARTESIAN_POINT ( 'NONE',  ( -31.00000000000003553, 8.000000000000000000, -21.00000000000000000 ) ) ;
#5918=PLANE ( 'NONE',  #9325 ) ;
#5930=LINE ( 'NONE', #7491, #6398 ) ;
#5943=DIRECTION ( 'NONE',  ( -0.000000000000000000, -1.000000000000000000, -0.000000000000000000 ) ) ;
#5949=EDGE_CURVE ( 'NONE', #1964, #11036, #9207, .T. ) ;
#5963=AXIS2_PLACEMENT_3D ( 'NONE', #16294, #11624, #382 ) ;
#5970=CARTESIAN_POINT ( 'NONE',  ( -35.00000000000000000, 19.00000000000000000, 20.99999999999999289 ) ) ;
#5988=EDGE_CURVE ( 'NONE', #10280, #19312, #3949, .T. ) ;
#5993=VECTOR ( 'NONE', #12830, 1000.000000000000000 ) ;
#6009=LINE ( 'NONE', #19904, #17592 ) ;
#6014=DIRECTION ( 'NONE',  ( 0.000000000000000000, 0.000000000000000000, -1.000000000000000000 ) ) ;
#6022=VERTEX_POINT ( 'NONE', #18573 ) ;
#6027=VECTOR ( 'NONE', #4298, 1000.000000000000000 ) ;
#6050=LINE ( 'NONE', #7498, #13446 ) ;
#6056=DIRECTION ( 'NONE',  ( 0.000000000000000000, 1.000000000000000000, 0.000000000000000000 ) ) ;
#6082=CYLINDRICAL_SURFACE ( 'NONE', #19736, 4.999999999999997335 ) ;
#6120=VERTEX_POINT ( 'NONE', #8376 ) ;
#6131=EDGE_CURVE ( 'NONE', #10847, #5205, #12812, .T. ) ;
#6155=DIRECTION ( 'NONE',  ( -1.000000000000000000, -0.000000000000000000, -0.000000000000000000 ) ) ;
#6171=CARTESIAN_POINT ( 'NONE',  ( -26.00000000000000000, 19.00000000000000000, 40.00000000000001421 ) ) ;
#6173=ORIENTED_EDGE ( 'NONE', *, *, #16313, .F. ) ;
#6181=CARTESIAN_POINT ( 'NONE',  ( 0.000000000000000000, 8.000000000000000000, -18.50000000000000000 ) ) ;
#6185=ORIENTED_EDGE ( 'NONE', *, *, #1070, .T. ) ;
#6189=DIRECTION ( 'NONE',  ( 0.000000000000000000, 0.000000000000000000, -1.000000000000000000 ) ) ;
#6208=ADVANCED_FACE ( 'NONE', ( #7333 ), #721, .F. ) ;
#6223=CARTESIAN_POINT ( 'NONE',  ( -35.00000000000000000, 19.00000000000000000, 20.99999999999999289 ) ) ;
#6227=DIRECTION ( 'NONE',  ( 0.000000000000000000, 0.000000000000000000, 1.000000000000000000 ) ) ;
#6231=EDGE_CURVE ( 'NONE', #19590, #14619, #974, .T. ) ;
#6233=LINE ( 'NONE', #7780, #4415 ) ;
#6234=EDGE_LOOP ( 'NONE', ( #18626, #13037 ) ) ;
#6242=VERTEX_POINT ( 'NONE', #5889 ) ;
#6250=VECTOR ( 'NONE', #11625, 1000.000000000000000 ) ;
#6253=CARTESIAN_POINT ( 'NONE',  ( 0.000000000000000000, 19.00100000000000122, 0.000000000000000000 ) ) ;
#6256=DIRECTION ( 'NONE',  ( -0.000000000000000000, -1.000000000000000000, -0.000000000000000000 ) ) ;
#6265=CARTESIAN_POINT ( 'NONE',  ( 31.81980515339464333, 0.000000000000000000, 31.81980515339463622 ) ) ;
#6274=ORIENTED_EDGE ( 'NONE', *, *, #15171, .T. ) ;
#6375=ORIENTED_EDGE ( 'NONE', *, *, #3714, .F. ) ;
#6383=ADVANCED_FACE ( 'NONE', ( #5364 ), #6921, .T. ) ;
#6386=AXIS2_PLACEMENT_3D ( 'NONE', #15330, #8651, #18112 ) ;
#6398=VECTOR ( 'NONE', #12034, 1000.000000000000000 ) ;
#6412=CARTESIAN_POINT ( 'NONE',  ( -34.99999999999999289, 11.00000000000000000, -35.00000000000000711 ) ) ;
#6431=ORIENTED_EDGE ( 'NONE', *, *, #3211, .T. ) ;
#6435=LINE ( 'NONE', #6223, #15315 ) ;
#6462=CARTESIAN_POINT ( 'NONE',  ( 40.00000000000000711, 11.00000000000000000, 25.99999999999999645 ) ) ;
#6472=ORIENTED_EDGE ( 'NONE', *, *, #4379, .F. ) ;
#6473=CARTESIAN_POINT ( 'NONE',  ( 4.286263797015737285E-15, 0.000000000000000000, -35.00000000000000711 ) ) ;
#6484=DIRECTION ( 'NONE',  ( 1.000000000000000000, 0.000000000000000000, 0.000000000000000000 ) ) ;
#6487=DIRECTION ( 'NONE',  ( -0.000000000000000000, -1.000000000000000000, -0.000000000000000000 ) ) ;
#6491=ORIENTED_EDGE ( 'NONE', *, *, #10891, .T. ) ;
#6497=VERTEX_POINT ( 'NONE', #5775 ) ;
#6503=CYLINDRICAL_SURFACE ( 'NONE', #13379, 4.999999999999997335 ) ;
#6511=DIRECTION ( 'NONE',  ( 0.000000000000000000, 0.000000000000000000, -1.000000000000000000 ) ) ;
#6513=VERTEX_POINT ( 'NONE', #2658 ) ;
#6529=DIRECTION ( 'NONE',  ( -0.000000000000000000, -1.000000000000000000, -0.000000000000000000 ) ) ;
#6564=LINE ( 'NONE', #6786, #9292 ) ;
#6590=DIRECTION ( 'NONE',  ( 1.000000000000000000, 0.000000000000000000, -0.000000000000000000 ) ) ;
#6599=ORIENTED_EDGE ( 'NONE', *, *, #85, .F. ) ;
#6606=DIRECTION ( 'NONE',  ( -0.000000000000000000, 1.000000000000000000, -0.000000000000000000 ) ) ;
#6612=VECTOR ( 'NONE', #12064, 1000.000000000000000 ) ;
#6613=AXIS2_PLACEMENT_3D ( 'NONE', #17345, #3228, #9507 ) ;
#6614=VECTOR ( 'NONE', #13034, 1000.000000000000000 ) ;
#6640=CARTESIAN_POINT ( 'NONE',  ( 31.81980515339464333, 8.000000000000000000, 31.81980515339463622 ) ) ;
#6641=CARTESIAN_POINT ( 'NONE',  ( 31.00000000000000000, 19.00000000000000000, -31.00000000000000355 ) ) ;
#6650=CARTESIAN_POINT ( 'NONE',  ( 40.00000000000000711, 11.00000000000000000, -26.00000000000000355 ) ) ;
#6677=ORIENTED_EDGE ( 'NONE', *, *, #7535, .F. ) ;
#6680=VERTEX_POINT ( 'NONE', #12771 ) ;
#6685=VERTEX_POINT ( 'NONE', #9774 ) ;
#6691=DIRECTION ( 'NONE',  ( -0.000000000000000000, -1.000000000000000000, -0.000000000000000000 ) ) ;
#6714=VECTOR ( 'NONE', #10887, 1000.000000000000000 ) ;
#6725=AXIS2_PLACEMENT_3D ( 'NONE', #8102, #14379, #3767 ) ;
#6731=CIRCLE ( 'NONE', #15940, 3.300000000000000711 ) ;
#6760=DIRECTION ( 'NONE',  ( 0.000000000000000000, 0.000000000000000000, -1.000000000000000000 ) ) ;
#6764=CARTESIAN_POINT ( 'NONE',  ( 31.00000000000000000, 8.000000000000000000, -31.00000000000000355 ) ) ;
#6776=SURFACE_SIDE_STYLE ('',( #13246 ) ) ;
#6786=CARTESIAN_POINT ( 'NONE',  ( -31.81980515339462912, 8.000000000000000000, -28.51980515339464972 ) ) ;
#6789=DIRECTION ( 'NONE',  ( -0.000000000000000000, -1.000000000000000000, 0.000000000000000000 ) ) ;
#6810=VECTOR ( 'NONE', #7630, 1000.000000000000000 ) ;
#6817=ORIENTED_EDGE ( 'NONE', *, *, #85, .T. ) ;
#6818=ORIENTED_EDGE ( 'NONE', *, *, #9513, .T. ) ;
#6823=DIRECTION ( 'NONE',  ( 0.000000000000000000, 0.000000000000000000, -1.000000000000000000 ) ) ;
#6849=LINE ( 'NONE', #19073, #19225 ) ;
#6859=VECTOR ( 'NONE', #6484, 1000.000000000000000 ) ;
#6860=VERTEX_POINT ( 'NONE', #19525 ) ;
#6864=VERTEX_POINT ( 'NONE', #5845 ) ;
#6886=ORIENTED_EDGE ( 'NONE', *, *, #13913, .F. ) ;
#6889=LINE ( 'NONE', #13173, #9267 ) ;
#6890=DIRECTION ( 'NONE',  ( 0.000000000000000000, 0.000000000000000000, 1.000000000000000000 ) ) ;
#6895=ADVANCED_FACE ( 'NONE', ( #13677 ), #4689, .T. ) ;
#6905=FACE_BOUND ( 'NONE', #8194, .T. ) ;
#6921=CYLINDRICAL_SURFACE ( 'NONE', #1942, 10.00000000000000178 ) ;
#7018=CARTESIAN_POINT ( 'NONE',  ( 26.00000000000000355, 19.00000000000000000, -31.00000000000003908 ) ) ;
#7030=EDGE_CURVE ( 'NONE', #6860, #10847, #10290, .T. ) ;
#7032=ORIENTED_EDGE ( 'NONE', *, *, #19762, .F. ) ;
#7034=CARTESIAN_POINT ( 'NONE',  ( 21.00000000000000000, 19.00000000000000000, -31.00000000000003908 ) ) ;
#7036=EDGE_LOOP ( 'NONE', ( #2750, #19596, #3028, #12682 ) ) ;
#7039=ORIENTED_EDGE ( 'NONE', *, *, #19791, .T. ) ;
#7062=DIRECTION ( 'NONE',  ( 0.000000000000000000, 0.000000000000000000, 1.000000000000000000 ) ) ;
#7094=ORIENTED_EDGE ( 'NONE', *, *, #15439, .T. ) ;
#7097=EDGE_CURVE ( 'NONE', #3610, #15515, #8555, .T. ) ;
#7101=PLANE ( 'NONE',  #11258 ) ;
#7109=CYLINDRICAL_SURFACE ( 'NONE', #5963, 3.299999999999997158 ) ;
#7112=VECTOR ( 'NONE', #4284, 1000.000000000000000 ) ;
#7113=EDGE_CURVE ( 'NONE', #9509, #15515, #15138, .T. ) ;
#7138=VECTOR ( 'NONE', #1499, 1000.000000000000000 ) ;
#7143=VERTEX_POINT ( 'NONE', #803 ) ;
#7146=DIRECTION ( 'NONE',  ( 0.000000000000000000, 0.000000000000000000, -1.000000000000000000 ) ) ;
#7154=VECTOR ( 'NONE', #5332, 1000.000000000000000 ) ;
#7190=CARTESIAN_POINT ( 'NONE',  ( -20.99999999999999645, 8.000000000000000000, 35.00000000000001421 ) ) ;
#7240=LINE ( 'NONE', #4342, #13268 ) ;
#7244=DIRECTION ( 'NONE',  ( -0.000000000000000000, -1.000000000000000000, -0.000000000000000000 ) ) ;
#7246=CARTESIAN_POINT ( 'NONE',  ( -31.00000000000003553, 19.00000000000000000, 25.99999999999999645 ) ) ;
#7257=DIRECTION ( 'NONE',  ( 0.000000000000000000, 0.000000000000000000, -1.000000000000000000 ) ) ;
#7264=EDGE_CURVE ( 'NONE', #15515, #13110, #421, .T. ) ;
#7288=CARTESIAN_POINT ( 'NONE',  ( 35.00000000000000711, 19.00000000000000000, 20.99999999999999289 ) ) ;
#7326=ORIENTED_EDGE ( 'NONE', *, *, #5276, .T. ) ;
#7333=FACE_OUTER_BOUND ( 'NONE', #15392, .T. ) ;
#7336=DIRECTION ( 'NONE',  ( 0.000000000000000000, 0.000000000000000000, 1.000000000000000000 ) ) ;
#7360=CARTESIAN_POINT ( 'NONE',  ( 40.00000000000000711, 19.00000000000000000, 25.99999999999999645 ) ) ;
#7382=VECTOR ( 'NONE', #8798, 1000.000000000000000 ) ;
#7384=CARTESIAN_POINT ( 'NONE',  ( 40.00000000000000711, 11.00000000000000000, 34.99999999999997868 ) ) ;
#7385=ORIENTED_EDGE ( 'NONE', *, *, #13467, .F. ) ;
#7419=LINE ( 'NONE', #13497, #458 ) ;
#7435=CARTESIAN_POINT ( 'NONE',  ( 21.00000000000000000, 19.00000000000000000, 35.00000000000001421 ) ) ;
#7468=CARTESIAN_POINT ( 'NONE',  ( 31.81980515339464333, 0.000000000000000000, 28.51980515339463906 ) ) ;
#7491=CARTESIAN_POINT ( 'NONE',  ( -20.99999999999999645, 8.000000000000000000, 35.00000000000001421 ) ) ;
#7498=CARTESIAN_POINT ( 'NONE',  ( -20.99999999999999645, 19.00000000000000000, -35.00000000000000711 ) ) ;
#7505=ORIENTED_EDGE ( 'NONE', *, *, #13557, .F. ) ;
#7535=EDGE_CURVE ( 'NONE', #16867, #10095, #4545, .T. ) ;
#7536=ORIENTED_EDGE ( 'NONE', *, *, #17686, .F. ) ;
#7555=DIRECTION ( 'NONE',  ( -0.000000000000000000, -1.000000000000000000, -0.000000000000000000 ) ) ;
#7556=DIRECTION ( 'NONE',  ( 0.000000000000000000, 1.000000000000000000, 0.000000000000000000 ) ) ;
#7564=ORIENTED_EDGE ( 'NONE', *, *, #19057, .T. ) ;
#7567=CARTESIAN_POINT ( 'NONE',  ( -35.00000000000000000, 19.00000000000000000, -21.00000000000000000 ) ) ;
#7575=CARTESIAN_POINT ( 'NONE',  ( 34.99999999999997868, 8.000000000000000000, 40.00000000000000711 ) ) ;
#7595=AXIS2_PLACEMENT_3D ( 'NONE', #12728, #11863, #6760 ) ;
#7598=ORIENTED_EDGE ( 'NONE', *, *, #9777, .F. ) ;
#7621=AXIS2_PLACEMENT_3D ( 'NONE', #3998, #6056, #13488 ) ;
#7628=ORIENTED_EDGE ( 'NONE', *, *, #17686, .T. ) ;
#7629=ORIENTED_EDGE ( 'NONE', *, *, #16565, .F. ) ;
#7630=DIRECTION ( 'NONE',  ( -0.000000000000000000, -1.000000000000000000, -0.000000000000000000 ) ) ;
#7631=CARTESIAN_POINT ( 'NONE',  ( -26.00000000000000000, 19.00000000000000000, -40.00000000000000711 ) ) ;
#7654=CARTESIAN_POINT ( 'NONE',  ( -35.00000000000000000, 8.000000000000000000, -21.00000000000000000 ) ) ;
#7672=PLANE ( 'NONE',  #12986 ) ;
#7685=CARTESIAN_POINT ( 'NONE',  ( 0.000000000000000000, -3.000000000000000000, 0.000000000000000000 ) ) ;
#7746=DIRECTION ( 'NONE',  ( 0.000000000000000000, 1.000000000000000000, 0.000000000000000000 ) ) ;
#7751=DIRECTION ( 'NONE',  ( 1.000000000000000000, 0.000000000000000000, -0.000000000000000000 ) ) ;
#7778=CARTESIAN_POINT ( 'NONE',  ( -31.00000000000000000, 11.00000000000000000, -31.00000000000000000 ) ) ;
#7780=CARTESIAN_POINT ( 'NONE',  ( -20.99999999999999645, 19.00000000000000000, 31.00000000000003197 ) ) ;
#7783=ORIENTED_EDGE ( 'NONE', *, *, #3415, .F. ) ;
#7786=ORIENTED_EDGE ( 'NONE', *, *, #1277, .F. ) ;
#7792=VERTEX_POINT ( 'NONE', #11333 ) ;
#7804=VECTOR ( 'NONE', #10072, 1000.000000000000000 ) ;
#7812=EDGE_LOOP ( 'NONE', ( #8451, #2083 ) ) ;
#7850=ADVANCED_FACE ( 'NONE', ( #19646 ), #14635, .F. ) ;
#7853=EDGE_LOOP ( 'NONE', ( #1928, #2186, #953, #18457 ) ) ;
#7857=DIRECTION ( 'NONE',  ( 0.000000000000000000, 0.000000000000000000, 1.000000000000000000 ) ) ;
#7864=CARTESIAN_POINT ( 'NONE',  ( 31.00000000000000000, 19.00000000000000000, 30.99999999999999289 ) ) ;
#7878=ORIENTED_EDGE ( 'NONE', *, *, #1340, .T. ) ;
#7888=AXIS2_PLACEMENT_3D ( 'NONE', #7685, #15328, #1251 ) ;
#7897=CARTESIAN_POINT ( 'NONE',  ( 31.00000000000003553, 19.00000000000000000, 25.99999999999999645 ) ) ;
#7900=LINE ( 'NONE', #10892, #17770 ) ;
#7903=ADVANCED_FACE ( 'NONE', ( #20053 ), #19855, .F. ) ;
#7919=CIRCLE ( 'NONE', #19419, 10.00000000000000178 ) ;
#7923=DIRECTION ( 'NONE',  ( -0.000000000000000000, -1.000000000000000000, -0.000000000000000000 ) ) ;
#7926=LINE ( 'NONE', #14207, #12639 ) ;
#7935=VECTOR ( 'NONE', #904, 1000.000000000000000 ) ;
#7937=CARTESIAN_POINT ( 'NONE',  ( -20.99999999999999645, 19.00000000000000000, -31.00000000000003908 ) ) ;
#7940=DIRECTION ( 'NONE',  ( -1.000000000000000000, 0.000000000000000000, -0.000000000000000000 ) ) ;
#7941=PRODUCT ( 'Servo-Head', 'Servo-Head', '', ( #12828 ) ) ;
#7951=ORIENTED_EDGE ( 'NONE', *, *, #11567, .F. ) ;
#7995=EDGE_LOOP ( 'NONE', ( #1269, #15349 ) ) ;
#8005=DIRECTION ( 'NONE',  ( 0.000000000000000000, 0.000000000000000000, -1.000000000000000000 ) ) ;
#8007=ORIENTED_EDGE ( 'NONE', *, *, #9904, .F. ) ;
#8026=CARTESIAN_POINT ( 'NONE',  ( 34.99999999999997868, 11.00000000000000000, -40.00000000000000711 ) ) ;
#8031=EDGE_CURVE ( 'NONE', #13058, #5525, #11106, .T. ) ;
#8036=ORIENTED_EDGE ( 'NONE', *, *, #12152, .F. ) ;
#8042=DIRECTION ( 'NONE',  ( -0.000000000000000000, -0.000000000000000000, 1.000000000000000000 ) ) ;
#8046=CARTESIAN_POINT ( 'NONE',  ( -31.00000000000003197, 19.00000000000000000, -26.00000000000000355 ) ) ;
#8071=VECTOR ( 'NONE', #15722, 1000.000000000000000 ) ;
#8083=FACE_BOUND ( 'NONE', #6234, .T. ) ;
#8089=LINE ( 'NONE', #340, #17494 ) ;
#8102=CARTESIAN_POINT ( 'NONE',  ( -31.00000000000000000, 8.000000000000000000, -31.00000000000000000 ) ) ;
#8133=VECTOR ( 'NONE', #14709, 1000.000000000000000 ) ;
#8139=DIRECTION ( 'NONE',  ( 0.000000000000000000, 0.000000000000000000, 1.000000000000000000 ) ) ;
#8190=CARTESIAN_POINT ( 'NONE',  ( 0.000000000000000000, 19.00100000000000122, 0.000000000000000000 ) ) ;
#8194=EDGE_LOOP ( 'NONE', ( #11866, #12506 ) ) ;
#8199=AXIS2_PLACEMENT_3D ( 'NONE', #10757, #8814, #12014 ) ;
#8215=ORIENTED_EDGE ( 'NONE', *, *, #15711, .T. ) ;
#8234=DIRECTION ( 'NONE',  ( 1.000000000000000000, 0.000000000000000000, 0.000000000000000000 ) ) ;
#8238=EDGE_LOOP ( 'NONE', ( #3982, #16785, #17404, #2672, #12376, #5624, #6818, #15676, #10460, #8215, #8276, #3942, #7094, #12024, #12136, #10745 ) ) ;
#8260=LINE ( 'NONE', #9806, #20219 ) ;
#8273=DIRECTION ( 'NONE',  ( 0.000000000000000000, 0.000000000000000000, -1.000000000000000000 ) ) ;
#8276=ORIENTED_EDGE ( 'NONE', *, *, #2580, .T. ) ;
#8279=CARTESIAN_POINT ( 'NONE',  ( 4.286263797015737285E-15, -3.000000000000000000, -35.00000000000000711 ) ) ;
#8294=AXIS2_PLACEMENT_3D ( 'NONE', #6265, #168, #4511 ) ;
#8309=ORIENTED_EDGE ( 'NONE', *, *, #1277, .T. ) ;
#8337=CARTESIAN_POINT ( 'NONE',  ( -40.00000000000000000, 19.00000000000000000, -26.00000000000000355 ) ) ;
#8339=CARTESIAN_POINT ( 'NONE',  ( -20.99999999999999645, 8.000000000000000000, -35.00000000000000711 ) ) ;
#8346=ORIENTED_EDGE ( 'NONE', *, *, #17121, .T. ) ;
#8350=ORIENTED_EDGE ( 'NONE', *, *, #6131, .T. ) ;
#8365=DIRECTION ( 'NONE',  ( -1.000000000000000000, -0.000000000000000000, -0.000000000000000000 ) ) ;
#8376=CARTESIAN_POINT ( 'NONE',  ( 2.265596578422603396E-15, 8.000000000000000000, 18.50000000000000000 ) ) ;
#8391=ADVANCED_FACE ( 'NONE', ( #5416 ), #9745, .T. ) ;
#8425=CARTESIAN_POINT ( 'NONE',  ( 31.00000000000003908, 19.00000000000000000, -26.00000000000000355 ) ) ;
#8440=CARTESIAN_POINT ( 'NONE',  ( 31.00000000000003908, 19.00000000000000000, -26.00000000000000355 ) ) ;
#8447=CARTESIAN_POINT ( 'NONE',  ( 31.81980515339464333, 11.00000000000000000, 31.81980515339463622 ) ) ;
#8451=ORIENTED_EDGE ( 'NONE', *, *, #6231, .T. ) ;
#8454=ORIENTED_EDGE ( 'NONE', *, *, #19281, .T. ) ;
#8464=DIRECTION ( 'NONE',  ( 0.000000000000000000, 0.000000000000000000, 1.000000000000000000 ) ) ;
#8466=VERTEX_POINT ( 'NONE', #8587 ) ;
#8469=VERTEX_POINT ( 'NONE', #16661 ) ;
#8481=LINE ( 'NONE', #3851, #820 ) ;
#8506=DIRECTION ( 'NONE',  ( 0.000000000000000000, 0.000000000000000000, -1.000000000000000000 ) ) ;
#8513=LINE ( 'NONE', #10371, #8133 ) ;
#8514=VERTEX_POINT ( 'NONE', #18719 ) ;
#8521=LINE ( 'NONE', #281, #2088 ) ;
#8555=CIRCLE ( 'NONE', #18424, 4.999999999999997335 ) ;
#8556=CIRCLE ( 'NONE', #6613, 9.999999999999998224 ) ;
#8562=ADVANCED_FACE ( 'NONE', ( #20360 ), #10902, .F. ) ;
#8566=CARTESIAN_POINT ( 'NONE',  ( 31.81980515339464333, 8.000000000000000000, -28.51980515339463906 ) ) ;
#8576=AXIS2_PLACEMENT_3D ( 'NONE', #18330, #2666, #5662 ) ;
#8580=VERTEX_POINT ( 'NONE', #6473 ) ;
#8583=DIRECTION ( 'NONE',  ( 0.000000000000000000, 0.000000000000000000, -1.000000000000000000 ) ) ;
#8587=CARTESIAN_POINT ( 'NONE',  ( 35.00000000000000711, 19.00000000000000000, 20.99999999999999289 ) ) ;
#8602=ORIENTED_EDGE ( 'NONE', *, *, #8954, .F. ) ;
#8604=ORIENTED_EDGE ( 'NONE', *, *, #17597, .F. ) ;
#8630=ORIENTED_EDGE ( 'NONE', *, *, #4486, .T. ) ;
#8639=AXIS2_PLACEMENT_3D ( 'NONE', #11704, #1886, #14576 ) ;
#8651=DIRECTION ( 'NONE',  ( -0.000000000000000000, -1.000000000000000000, -0.000000000000000000 ) ) ;
#8666=ORIENTED_EDGE ( 'NONE', *, *, #11842, .F. ) ;
#8678=LINE ( 'NONE', #12085, #16888 ) ;
#8692=EDGE_CURVE ( 'NONE', #715, #6680, #6889, .T. ) ;
#8699=VECTOR ( 'NONE', #8365, 1000.000000000000000 ) ;
#8759=AXIS2_PLACEMENT_3D ( 'NONE', #17106, #2986, #9275 ) ;
#8781=ORIENTED_EDGE ( 'NONE', *, *, #14175, .T. ) ;
#8788=FACE_OUTER_BOUND ( 'NONE', #11907, .T. ) ;
#8793=CARTESIAN_POINT ( 'NONE',  ( 31.00000000000000000, 11.00000000000000000, -31.00000000000000355 ) ) ;
#8798=DIRECTION ( 'NONE',  ( -3.854941057726249437E-16, 0.000000000000000000, -1.000000000000000000 ) ) ;
#8808=CARTESIAN_POINT ( 'NONE',  ( -40.00000000000000000, 19.00000000000000000, 25.99999999999999645 ) ) ;
#8814=DIRECTION ( 'NONE',  ( 0.000000000000000000, 1.000000000000000000, 0.000000000000000000 ) ) ;
#8817=DIRECTION ( 'NONE',  ( 0.000000000000000000, -0.000000000000000000, -1.000000000000000000 ) ) ;
#8821=ORIENTED_EDGE ( 'NONE', *, *, #14555, .T. ) ;
#8844=EDGE_LOOP ( 'NONE', ( #1876, #9520, #617, #3449 ) ) ;
#8865=CARTESIAN_POINT ( 'NONE',  ( -31.00000000000006395, 8.000000000000000000, 20.99999999999998934 ) ) ;
#8883=CARTESIAN_POINT ( 'NONE',  ( 31.81980515339464333, 11.00000000000000000, -31.81980515339463622 ) ) ;
#8890=EDGE_CURVE ( 'NONE', #13589, #13719, #15208, .T. ) ;
#8912=VERTEX_POINT ( 'NONE', #18294 ) ;
#8930=CARTESIAN_POINT ( 'NONE',  ( 35.00000000000000711, 8.000000000000000000, -21.00000000000000355 ) ) ;
#8932=CARTESIAN_POINT ( 'NONE',  ( -26.00000000000000000, 11.00000000000000000, -40.00000000000000711 ) ) ;
#8953=CIRCLE ( 'NONE', #15553, 9.999999999999998224 ) ;
#8954=EDGE_CURVE ( 'NONE', #8514, #4609, #16862, .T. ) ;
#8982=DIRECTION ( 'NONE',  ( 0.000000000000000000, 0.000000000000000000, 1.000000000000000000 ) ) ;
#8986=AXIS2_PLACEMENT_3D ( 'NONE', #16825, #15069, #19886 ) ;
#8996=CARTESIAN_POINT ( 'NONE',  ( -20.99999999999999645, 19.00000000000000000, 35.00000000000001421 ) ) ;
#9002=DIRECTION ( 'NONE',  ( 0.000000000000000000, 0.000000000000000000, -1.000000000000000000 ) ) ;
#9007=AXIS2_PLACEMENT_3D ( 'NONE', #1547, #3007, #7857 ) ;
#9030=DIRECTION ( 'NONE',  ( -0.000000000000000000, -1.000000000000000000, -0.000000000000000000 ) ) ;
#9042=EDGE_CURVE ( 'NONE', #19183, #16269, #4682, .T. ) ;
#9081=VERTEX_POINT ( 'NONE', #15736 ) ;
#9089=PRODUCT_DEFINITION_SHAPE ( 'NONE', 'NONE',  #158 ) ;
#9103=EDGE_CURVE ( 'NONE', #8514, #6685, #14157, .T. ) ;
#9104=DIRECTION ( 'NONE',  ( -0.000000000000000000, -1.000000000000000000, -0.000000000000000000 ) ) ;
#9117=ORIENTED_EDGE ( 'NONE', *, *, #19714, .F. ) ;
#9137=CARTESIAN_POINT ( 'NONE',  ( 34.99999999999997868, 11.00000000000000000, 40.00000000000000711 ) ) ;
#9149=CARTESIAN_POINT ( 'NONE',  ( -20.99999999999999645, 19.00000000000000000, -35.00000000000000711 ) ) ;
#9167=ORIENTED_EDGE ( 'NONE', *, *, #15189, .T. ) ;
#9191=CARTESIAN_POINT ( 'NONE',  ( 21.00000000000000000, 8.000000000000000000, 31.00000000000006395 ) ) ;
#9198=LINE ( 'NONE', #3012, #1634 ) ;
#9199=LINE ( 'NONE', #20229, #486 ) ;
#9202=ORIENTED_EDGE ( 'NONE', *, *, #18355, .T. ) ;
#9207=CIRCLE ( 'NONE', #2278, 10.00000000000000178 ) ;
#9225=DIRECTION ( 'NONE',  ( 0.000000000000000000, 0.000000000000000000, -1.000000000000000000 ) ) ;
#9241=ORIENTED_EDGE ( 'NONE', *, *, #2608, .T. ) ;
#9257=EDGE_CURVE ( 'NONE', #1902, #9830, #16727, .T. ) ;
#9260=EDGE_CURVE ( 'NONE', #4676, #4285, #12711, .T. ) ;
#9267=VECTOR ( 'NONE', #19422, 1000.000000000000000 ) ;
#9275=DIRECTION ( 'NONE',  ( 0.000000000000000000, 0.000000000000000000, -1.000000000000000000 ) ) ;
#9284=DIRECTION ( 'NONE',  ( 0.000000000000000000, 1.000000000000000000, 0.000000000000000000 ) ) ;
#9292=VECTOR ( 'NONE', #9638, 1000.000000000000000 ) ;
#9293=VECTOR ( 'NONE', #12768, 1000.000000000000000 ) ;
#9299=FACE_OUTER_BOUND ( 'NONE', #86, .T. ) ;
#9303=VECTOR ( 'NONE', #6511, 1000.000000000000000 ) ;
#9308=ORIENTED_EDGE ( 'NONE', *, *, #19223, .F. ) ;
#9315=VERTEX_POINT ( 'NONE', #3384 ) ;
#9319=ORIENTED_EDGE ( 'NONE', *, *, #914, .F. ) ;
#9320=CIRCLE ( 'NONE', #11292, 4.999999999999997335 ) ;
#9322=DIRECTION ( 'NONE',  ( -0.000000000000000000, -1.000000000000000000, -0.000000000000000000 ) ) ;
#9325=AXIS2_PLACEMENT_3D ( 'NONE', #10761, #16958, #8817 ) ;
#9338=CARTESIAN_POINT ( 'NONE',  ( -20.99999999999999645, 8.000000000000000000, -31.00000000000003553 ) ) ;
#9358=EDGE_CURVE ( 'NONE', #12917, #15939, #5468, .T. ) ;
#9373=EDGE_CURVE ( 'NONE', #14625, #18451, #2780, .T. ) ;
#9382=ORIENTED_EDGE ( 'NONE', *, *, #14045, .T. ) ;
#9410=ADVANCED_FACE ( 'NONE', ( #3295 ), #16104, .T. ) ;
#9417=PLANE ( 'NONE',  #5884 ) ;
#9419=CARTESIAN_POINT ( 'NONE',  ( 40.00000000000000711, 8.000000000000000000, 34.99999999999997868 ) ) ;
#9421=ORIENTED_EDGE ( 'NONE', *, *, #1834, .T. ) ;
#9430=DIRECTION ( 'NONE',  ( -0.000000000000000000, -1.000000000000000000, -0.000000000000000000 ) ) ;
#9434=LINE ( 'NONE', #13973, #10368 ) ;
#9460=DIRECTION ( 'NONE',  ( 0.000000000000000000, -1.000000000000000000, 0.000000000000000000 ) ) ;
#9474=ORIENTED_EDGE ( 'NONE', *, *, #173, .F. ) ;
#9475=EDGE_LOOP ( 'NONE', ( #9989, #14707, #14960, #4147, #11201, #5255, #9202, #19826, #7628, #8346, #19710, #10511, #6185, #5649, #9740, #8350 ) ) ;
#9476=LINE ( 'NONE', #12692, #12740 ) ;
#9507=DIRECTION ( 'NONE',  ( 0.000000000000000000, 0.000000000000000000, 1.000000000000000000 ) ) ;
#9509=VERTEX_POINT ( 'NONE', #3198 ) ;
#9511=DIRECTION ( 'NONE',  ( 1.000000000000000000, -0.000000000000000000, 0.000000000000000000 ) ) ;
#9513=EDGE_CURVE ( 'NONE', #14625, #13058, #9476, .T. ) ;
#9520=ORIENTED_EDGE ( 'NONE', *, *, #13133, .F. ) ;
#9535=CARTESIAN_POINT ( 'NONE',  ( 35.00000000000000711, 19.00000000000000000, 20.99999999999999289 ) ) ;
#9557=CARTESIAN_POINT ( 'NONE',  ( 31.81980515339464333, 8.000000000000000000, -31.81980515339463622 ) ) ;
#9564=VERTEX_POINT ( 'NONE', #19549 ) ;
#9568=DIRECTION ( 'NONE',  ( 1.000000000000000000, 0.000000000000000000, 0.000000000000000000 ) ) ;
#9596=DIRECTION ( 'NONE',  ( 0.000000000000000000, 0.000000000000000000, -1.000000000000000000 ) ) ;
#9617=CARTESIAN_POINT ( 'NONE',  ( 35.00000000000000711, 8.000000000000000000, 20.99999999999999289 ) ) ;
#9625=CARTESIAN_POINT ( 'NONE',  ( 31.00000000000000000, 19.00000000000000000, -31.00000000000000355 ) ) ;
#9630=LINE ( 'NONE', #15844, #5689 ) ;
#9631=EDGE_CURVE ( 'NONE', #3967, #6864, #20049, .T. ) ;
#9638=DIRECTION ( 'NONE',  ( -0.000000000000000000, -1.000000000000000000, -0.000000000000000000 ) ) ;
#9642=CARTESIAN_POINT ( 'NONE',  ( 34.99999999999997868, 0.000000000000000000, 40.00000000000000711 ) ) ;
#9648=LINE ( 'NONE', #15973, #15994 ) ;
#9660=ADVANCED_FACE ( 'NONE', ( #16998 ), #2853, .T. ) ;
#9673=ORIENTED_EDGE ( 'NONE', *, *, #14322, .F. ) ;
#9674=VECTOR ( 'NONE', #18771, 1000.000000000000000 ) ;
#9675=VECTOR ( 'NONE', #8042, 1000.000000000000000 ) ;
#9677=VERTEX_POINT ( 'NONE', #5031 ) ;
#9711=CARTESIAN_POINT ( 'NONE',  ( 26.00000000000000355, 11.00000000000000000, -40.00000000000000711 ) ) ;
#9713=ORIENTED_EDGE ( 'NONE', *, *, #3415, .T. ) ;
#9725=CARTESIAN_POINT ( 'NONE',  ( 31.81980515339464333, 0.000000000000000000, -35.11980515339463693 ) ) ;
#9727=CARTESIAN_POINT ( 'NONE',  ( 31.81980515339464333, 11.00000000000000000, -28.51980515339463906 ) ) ;
#9740=ORIENTED_EDGE ( 'NONE', *, *, #9904, .T. ) ;
#9745=PLANE ( 'NONE',  #8639 ) ;
#9747=FACE_OUTER_BOUND ( 'NONE', #10608, .T. ) ;
#9774=CARTESIAN_POINT ( 'NONE',  ( 40.00000000000000711, 0.000000000000000000, 34.99999999999997868 ) ) ;
#9777=EDGE_CURVE ( 'NONE', #9081, #17030, #17993, .T. ) ;
#9796=DIRECTION ( 'NONE',  ( -0.000000000000000000, -1.000000000000000000, -0.000000000000000000 ) ) ;
#9806=CARTESIAN_POINT ( 'NONE',  ( -31.81980515339462912, 8.000000000000000000, 35.11980515339465825 ) ) ;
#9808=EDGE_CURVE ( 'NONE', #9677, #19312, #8513, .T. ) ;
#9816=CARTESIAN_POINT ( 'NONE',  ( 40.00000000000000711, 11.00000000000000000, 25.99999999999999645 ) ) ;
#9829=DIRECTION ( 'NONE',  ( 0.000000000000000000, 0.000000000000000000, -1.000000000000000000 ) ) ;
#9830=VERTEX_POINT ( 'NONE', #14907 ) ;
#9853=CARTESIAN_POINT ( 'NONE',  ( -31.00000000000000000, 19.00000000000000000, -31.00000000000000000 ) ) ;
#9862=VERTEX_POINT ( 'NONE', #19623 ) ;
#9885=EDGE_CURVE ( 'NONE', #4994, #758, #5493, .T. ) ;
#9894=EDGE_CURVE ( 'NONE', #6680, #4513, #12406, .T. ) ;
#9897=CARTESIAN_POINT ( 'NONE',  ( -34.99999999999996447, 11.00000000000000000, -40.00000000000000711 ) ) ;
#9899=CARTESIAN_POINT ( 'NONE',  ( 0.000000000000000000, -3.000000000000000000, 0.000000000000000000 ) ) ;
#9904=EDGE_CURVE ( 'NONE', #9830, #10847, #580, .T. ) ;
#9929=DIRECTION ( 'NONE',  ( 0.000000000000000000, 1.000000000000000000, 0.000000000000000000 ) ) ;
#9930=PLANE ( 'NONE',  #7595 ) ;
#9937=VECTOR ( 'NONE', #5137, 1000.000000000000000 ) ;
#9946=DIRECTION ( 'NONE',  ( 0.000000000000000000, 0.000000000000000000, -1.000000000000000000 ) ) ;
#9956=CARTESIAN_POINT ( 'NONE',  ( 21.00000000000000000, 8.000000000000000000, 35.00000000000001421 ) ) ;
#9981=DIRECTION ( 'NONE',  ( 0.000000000000000000, 0.000000000000000000, 1.000000000000000000 ) ) ;
#9984=VERTEX_POINT ( 'NONE', #16772 ) ;
#9987=ORIENTED_EDGE ( 'NONE', *, *, #5276, .F. ) ;
#9989=ORIENTED_EDGE ( 'NONE', *, *, #2492, .T. ) ;
#10018=ADVANCED_FACE ( 'NONE', ( #16973 ), #18606, .T. ) ;
#10019=LINE ( 'NONE', #9816, #12660 ) ;
#10065=EDGE_CURVE ( 'NONE', #975, #5571, #5930, .T. ) ;
#10072=DIRECTION ( 'NONE',  ( -0.000000000000000000, -1.000000000000000000, -0.000000000000000000 ) ) ;
#10088=CARTESIAN_POINT ( 'NONE',  ( 25.99999999999999645, 11.00000000000000000, 40.00000000000000711 ) ) ;
#10093=ORIENTED_EDGE ( 'NONE', *, *, #19556, .F. ) ;
#10095=VERTEX_POINT ( 'NONE', #19214 ) ;
#10129=DIRECTION ( 'NONE',  ( -3.854941057726247958E-16, 0.000000000000000000, 1.000000000000000000 ) ) ;
#10133=CARTESIAN_POINT ( 'NONE',  ( 26.00000000000000000, 19.00000000000000000, -40.00000000000000711 ) ) ;
#10140=ORIENTED_EDGE ( 'NONE', *, *, #18304, .F. ) ;
#10142=CARTESIAN_POINT ( 'NONE',  ( 31.81980515339464333, 8.000000000000000000, -31.81980515339463622 ) ) ;
#10175=DIRECTION ( 'NONE',  ( 1.000000000000000000, 0.000000000000000000, 0.000000000000000000 ) ) ;
#10190=CARTESIAN_POINT ( 'NONE',  ( -39.99999999999999289, 8.000000000000000000, -34.99999999999997868 ) ) ;
#10192=DIRECTION ( 'NONE',  ( -1.000000000000000000, -0.000000000000000000, -0.000000000000000000 ) ) ;
#10203=ORIENTED_EDGE ( 'NONE', *, *, #11567, .T. ) ;
#10211=CARTESIAN_POINT ( 'NONE',  ( 31.00000000000003553, 19.00000000000000000, 25.99999999999999645 ) ) ;
#10226=ADVANCED_FACE ( 'NONE', ( #5508 ), #10233, .T. ) ;
#10229=ORIENTED_EDGE ( 'NONE', *, *, #11254, .F. ) ;
#10233=CYLINDRICAL_SURFACE ( 'NONE', #1755, 4.999999999999997335 ) ;
#10239=EDGE_CURVE ( 'NONE', #17989, #18007, #17766, .T. ) ;
#10242=CARTESIAN_POINT ( 'NONE',  ( -20.99999999999999645, 8.000000000000000000, 31.00000000000003197 ) ) ;
#10245=CARTESIAN_POINT ( 'NONE',  ( -31.81980515339462912, 0.000000000000000000, -28.51980515339464972 ) ) ;
#10250=EDGE_CURVE ( 'NONE', #53, #5039, #17254, .T. ) ;
#10252=ORIENTED_EDGE ( 'NONE', *, *, #3881, .T. ) ;
#10260=EDGE_LOOP ( 'NONE', ( #2595, #6431 ) ) ;
#10263=VERTEX_POINT ( 'NONE', #9191 ) ;
#10264=EDGE_CURVE ( 'NONE', #9564, #7792, #1223, .T. ) ;
#10270=CARTESIAN_POINT ( 'NONE',  ( -26.00000000000000355, 11.00000000000000000, 31.00000000000003553 ) ) ;
#10280=VERTEX_POINT ( 'NONE', #7468 ) ;
#10281=DIRECTION ( 'NONE',  ( 0.000000000000000000, 0.000000000000000000, -1.000000000000000000 ) ) ;
#10288=EDGE_CURVE ( 'NONE', #2504, #10095, #20107, .T. ) ;
#10290=LINE ( 'NONE', #11851, #15 ) ;
#10292=EDGE_CURVE ( 'NONE', #13536, #5483, #6009, .T. ) ;
#10304=CARTESIAN_POINT ( 'NONE',  ( 31.00000000000003553, 11.00000000000000000, 25.99999999999999645 ) ) ;
#10342=PLANE ( 'NONE',  #12018 ) ;
#10355=EDGE_LOOP ( 'NONE', ( #11098, #10229, #17101, #5720 ) ) ;
#10358=VECTOR ( 'NONE', #17527, 1000.000000000000000 ) ;
#10359=ADVANCED_FACE ( 'NONE', ( #2601 ), #10342, .T. ) ;
#10368=VECTOR ( 'NONE', #15840, 1000.000000000000000 ) ;
#10371=CARTESIAN_POINT ( 'NONE',  ( 31.81980515339464333, 8.000000000000000000, 35.11980515339463693 ) ) ;
#10382=AXIS2_PLACEMENT_3D ( 'NONE', #15723, #16035, #9596 ) ;
#10385=DIRECTION ( 'NONE',  ( 0.000000000000000000, 1.000000000000000000, -0.000000000000000000 ) ) ;
#10390=AXIS2_PLACEMENT_3D ( 'NONE', #1643, #3223, #4780 ) ;
#10394=EDGE_LOOP ( 'NONE', ( #4685, #18624, #17201, #3733 ) ) ;
#10398=EDGE_CURVE ( 'NONE', #16269, #7792, #5816, .T. ) ;
#10401=VECTOR ( 'NONE', #17842, 1000.000000000000000 ) ;
#10414=CARTESIAN_POINT ( 'NONE',  ( 21.00000000000000000, 19.00000000000000000, -31.00000000000003908 ) ) ;
#10434=CARTESIAN_POINT ( 'NONE',  ( 31.00000000000003908, 19.00000000000000000, -26.00000000000000355 ) ) ;
#10438=CARTESIAN_POINT ( 'NONE',  ( -31.00000000000006395, 19.00000000000000000, 20.99999999999998934 ) ) ;
#10446=ORIENTED_EDGE ( 'NONE', *, *, #2027, .F. ) ;
#10460=ORIENTED_EDGE ( 'NONE', *, *, #1066, .T. ) ;
#10476=CARTESIAN_POINT ( 'NONE',  ( 21.00000000000000000, 19.00000000000000000, 35.00000000000001421 ) ) ;
#10478=DIRECTION ( 'NONE',  ( 0.000000000000000000, -0.000000000000000000, 1.000000000000000000 ) ) ;
#10503=CARTESIAN_POINT ( 'NONE',  ( 40.00000000000000711, 0.000000000000000000, -34.99999999999997868 ) ) ;
#10506=EDGE_CURVE ( 'NONE', #4609, #17030, #10019, .T. ) ;
#10507=CIRCLE ( 'NONE', #2918, 3.299999999999997158 ) ;
#10509=ORIENTED_EDGE ( 'NONE', *, *, #15577, .F. ) ;
#10510=VERTEX_POINT ( 'NONE', #5190 ) ;
#10511=ORIENTED_EDGE ( 'NONE', *, *, #2027, .T. ) ;
#10512=ADVANCED_FACE ( 'NONE', ( #19377 ), #1954, .T. ) ;
#10518=DIRECTION ( 'NONE',  ( -1.000000000000000000, 0.000000000000000000, 0.000000000000000000 ) ) ;
#10521=APPLICATION_CONTEXT ( 'automotive_design' ) ;
#10548=EDGE_CURVE ( 'NONE', #18451, #5238, #13706, .T. ) ;
#10561=VECTOR ( 'NONE', #15253, 1000.000000000000000 ) ;
#10565=CIRCLE ( 'NONE', #1647, 3.299999999999997158 ) ;
#10566=VECTOR ( 'NONE', #11146, 1000.000000000000000 ) ;
#10581=CARTESIAN_POINT ( 'NONE',  ( 35.00000000000000711, 0.000000000000000000, -35.00000000000000711 ) ) ;
#10595=DIRECTION ( 'NONE',  ( 0.000000000000000000, 0.000000000000000000, -1.000000000000000000 ) ) ;
#10608=EDGE_LOOP ( 'NONE', ( #12407, #17617, #18574, #7385 ) ) ;
#10611=VECTOR ( 'NONE', #11878, 1000.000000000000000 ) ;
#10620=DIRECTION ( 'NONE',  ( 0.000000000000000000, 1.000000000000000000, 0.000000000000000000 ) ) ;
#10640=CIRCLE ( 'NONE', #18531, 5.000000000000000888 ) ;
#10677=LINE ( 'NONE', #15538, #15795 ) ;
#10690=DIRECTION ( 'NONE',  ( 0.000000000000000000, 0.000000000000000000, -1.000000000000000000 ) ) ;
#10696=ORIENTED_EDGE ( 'NONE', *, *, #13145, .F. ) ;
#10736=FACE_OUTER_BOUND ( 'NONE', #15151, .T. ) ;
#10744=EDGE_CURVE ( 'NONE', #7792, #17989, #12345, .T. ) ;
#10745=ORIENTED_EDGE ( 'NONE', *, *, #20075, .T. ) ;
#10757=CARTESIAN_POINT ( 'NONE',  ( -31.81980515339462912, 11.00000000000000000, 31.81980515339465043 ) ) ;
#10761=CARTESIAN_POINT ( 'NONE',  ( 35.00000000000000711, 8.000000000000000000, -35.00000000000000711 ) ) ;
#10763=ORIENTED_EDGE ( 'NONE', *, *, #10548, .F. ) ;
#10795=ORIENTED_EDGE ( 'NONE', *, *, #502, .T. ) ;
#10800=ORIENTED_EDGE ( 'NONE', *, *, #17080, .T. ) ;
#10816=ORIENTED_EDGE ( 'NONE', *, *, #19678, .F. ) ;
#10817=ORIENTED_EDGE ( 'NONE', *, *, #9808, .F. ) ;
#10826=FACE_OUTER_BOUND ( 'NONE', #5232, .T. ) ;
#10832=AXIS2_PLACEMENT_3D ( 'NONE', #18245, #10620, #4157 ) ;
#10847=VERTEX_POINT ( 'NONE', #12215 ) ;
#10850=LINE ( 'NONE', #12721, #8071 ) ;
#10880=CARTESIAN_POINT ( 'NONE',  ( -20.99999999999999645, 19.00000000000000000, -31.00000000000003908 ) ) ;
#10887=DIRECTION ( 'NONE',  ( 0.000000000000000000, 0.000000000000000000, -1.000000000000000000 ) ) ;
#10891=EDGE_CURVE ( 'NONE', #12591, #10263, #10677, .T. ) ;
#10892=CARTESIAN_POINT ( 'NONE',  ( -34.99999999999996447, 0.000000000000000000, -40.00000000000000711 ) ) ;
#10902=PLANE ( 'NONE',  #4666 ) ;
#10906=CARTESIAN_POINT ( 'NONE',  ( -31.81980515339462912, 11.00000000000000000, -31.81980515339465043 ) ) ;
#10926=CIRCLE ( 'NONE', #7621, 4.999999999999997335 ) ;
#10953=DIRECTION ( 'NONE',  ( 0.000000000000000000, 1.000000000000000000, 0.000000000000000000 ) ) ;
#10961=FACE_OUTER_BOUND ( 'NONE', #15519, .T. ) ;
#10971=ADVANCED_FACE ( 'NONE', ( #1796 ), #12959, .T. ) ;
#10984=COLOUR_RGB ( '', 0.09019608, 0.27058824, 0.51372549) ;
#10987=EDGE_LOOP ( 'NONE', ( #2024, #16377, #11247, #2653 ) ) ;
#10991=DIRECTION ( 'NONE',  ( -0.000000000000000000, -1.000000000000000000, -0.000000000000000000 ) ) ;
#11004=DIRECTION ( 'NONE',  ( 0.000000000000000000, 0.000000000000000000, 1.000000000000000000 ) ) ;
#11032=VECTOR ( 'NONE', #10192, 1000.000000000000000 ) ;
#11036=VERTEX_POINT ( 'NONE', #10242 ) ;
#11057=ORIENTED_EDGE ( 'NONE', *, *, #15439, .F. ) ;
#11084=LINE ( 'NONE', #20253, #13994 ) ;
#11092=CYLINDRICAL_SURFACE ( 'NONE', #2751, 3.300000000000000711 ) ;
#11098=ORIENTED_EDGE ( 'NONE', *, *, #2492, .F. ) ;
#11103=ADVANCED_FACE ( 'NONE', ( #18581 ), #942, .T. ) ;
#11106=LINE ( 'NONE', #15984, #9293 ) ;
#11111=CARTESIAN_POINT ( 'NONE',  ( -31.81980515339462912, 0.000000000000000000, -31.81980515339465043 ) ) ;
#11113=DIRECTION ( 'NONE',  ( 0.000000000000000000, 0.000000000000000000, -1.000000000000000000 ) ) ;
#11131=CARTESIAN_POINT ( 'NONE',  ( 31.81980515339464333, 8.000000000000000000, 31.81980515339463622 ) ) ;
#11136=DIRECTION ( 'NONE',  ( 0.000000000000000000, 0.000000000000000000, 1.000000000000000000 ) ) ;
#11146=DIRECTION ( 'NONE',  ( -0.000000000000000000, -0.000000000000000000, 1.000000000000000000 ) ) ;
#11160=LINE ( 'NONE', #15052, #16833 ) ;
#11198=EDGE_LOOP ( 'NONE', ( #1239, #16051, #276, #15671 ) ) ;
#11201=ORIENTED_EDGE ( 'NONE', *, *, #4099, .T. ) ;
#11244=VERTEX_POINT ( 'NONE', #1650 ) ;
#11247=ORIENTED_EDGE ( 'NONE', *, *, #8692, .T. ) ;
#11254=EDGE_CURVE ( 'NONE', #5413, #5205, #15918, .T. ) ;
#11258=AXIS2_PLACEMENT_3D ( 'NONE', #8440, #16184, #19429 ) ;
#11261=CARTESIAN_POINT ( 'NONE',  ( 31.00000000000000000, 11.00000000000000000, -26.00000000000000355 ) ) ;
#11286=LINE ( 'NONE', #9535, #6714 ) ;
#11289=ORIENTED_EDGE ( 'NONE', *, *, #9894, .F. ) ;
#11292=AXIS2_PLACEMENT_3D ( 'NONE', #13792, #12070, #19965 ) ;
#11295=ORIENTED_EDGE ( 'NONE', *, *, #5155, .T. ) ;
#11323=ORIENTED_EDGE ( 'NONE', *, *, #9885, .T. ) ;
#11328=AXIS2_PLACEMENT_3D ( 'NONE', #16022, #1948, #4964 ) ;
#11333=CARTESIAN_POINT ( 'NONE',  ( 26.00000000000000355, 11.00000000000000000, -31.00000000000004263 ) ) ;
#11340=DIRECTION ( 'NONE',  ( 0.000000000000000000, 0.000000000000000000, -1.000000000000000000 ) ) ;
#11373=ORIENTED_EDGE ( 'NONE', *, *, #10239, .T. ) ;
#11426=FACE_OUTER_BOUND ( 'NONE', #3341, .T. ) ;
#11428=FACE_OUTER_BOUND ( 'NONE', #14314, .T. ) ;
#11430=LINE ( 'NONE', #10088, #1999 ) ;
#11473=DIRECTION ( 'NONE',  ( -0.000000000000000000, -1.000000000000000000, -0.000000000000000000 ) ) ;
#11476=EDGE_LOOP ( 'NONE', ( #834, #11668, #15738, #17035, #15591, #19973, #1840, #3746 ) ) ;
#11498=CARTESIAN_POINT ( 'NONE',  ( -26.00000000000000000, 19.00000000000000000, -31.00000000000003908 ) ) ;
#11519=EDGE_CURVE ( 'NONE', #16481, #17989, #13438, .T. ) ;
#11521=CARTESIAN_POINT ( 'NONE',  ( -34.99999999999996447, 8.000000000000000000, 40.00000000000000711 ) ) ;
#11538=ADVANCED_FACE ( 'NONE', ( #10736, #19674 ), #18139, .T. ) ;
#11556=DIRECTION ( 'NONE',  ( -0.000000000000000000, -1.000000000000000000, -0.000000000000000000 ) ) ;
#11567=EDGE_CURVE ( 'NONE', #20055, #17762, #212, .T. ) ;
#11571=DIRECTION ( 'NONE',  ( 0.000000000000000000, 0.000000000000000000, -1.000000000000000000 ) ) ;
#11580=CARTESIAN_POINT ( 'NONE',  ( 21.00000000000000000, 19.00000000000000000, -31.00000000000003908 ) ) ;
#11589=DIRECTION ( 'NONE',  ( 0.000000000000000000, 1.000000000000000000, -0.000000000000000000 ) ) ;
#11602=ORIENTED_EDGE ( 'NONE', *, *, #8954, .T. ) ;
#11624=DIRECTION ( 'NONE',  ( -0.000000000000000000, -1.000000000000000000, -0.000000000000000000 ) ) ;
#11625=DIRECTION ( 'NONE',  ( -0.000000000000000000, -1.000000000000000000, -0.000000000000000000 ) ) ;
#11659=VECTOR ( 'NONE', #1018, 1000.000000000000000 ) ;
#11660=ORIENTED_EDGE ( 'NONE', *, *, #17630, .F. ) ;
#11668=ORIENTED_EDGE ( 'NONE', *, *, #17336, .F. ) ;
#11702=LINE ( 'NONE', #8996, #1079 ) ;
#11704=CARTESIAN_POINT ( 'NONE',  ( -35.00000000000000000, 19.00000000000000000, 20.99999999999999289 ) ) ;
#11788=VECTOR ( 'NONE', #3438, 1000.000000000000000 ) ;
#11812=ADVANCED_FACE ( 'NONE', ( #14952, #4322 ), #15051, .T. ) ;
#11822=CARTESIAN_POINT ( 'NONE',  ( 31.81980515339464333, 11.00000000000000000, -31.81980515339463622 ) ) ;
#11842=EDGE_CURVE ( 'NONE', #9862, #3967, #19967, .T. ) ;
#11851=CARTESIAN_POINT ( 'NONE',  ( 21.00000000000000000, 19.00000000000000000, -35.00000000000000711 ) ) ;
#11858=DIRECTION ( 'NONE',  ( -0.000000000000000000, -1.000000000000000000, -0.000000000000000000 ) ) ;
#11862=AXIS2_PLACEMENT_3D ( 'NONE', #1027, #13738, #2806 ) ;
#11863=DIRECTION ( 'NONE',  ( 1.000000000000000000, -0.000000000000000000, 0.000000000000000000 ) ) ;
#11866=ORIENTED_EDGE ( 'NONE', *, *, #12152, .T. ) ;
#11870=ORIENTED_EDGE ( 'NONE', *, *, #9373, .T. ) ;
#11878=DIRECTION ( 'NONE',  ( -1.000000000000000000, -0.000000000000000000, -0.000000000000000000 ) ) ;
#11888=AXIS2_PLACEMENT_3D ( 'NONE', #4673, #9511, #15728 ) ;
#11899=CARTESIAN_POINT ( 'NONE',  ( 21.00000000000000000, 8.000000000000000000, 35.00000000000001421 ) ) ;
#11907=EDGE_LOOP ( 'NONE', ( #19515, #15782, #2778, #9421 ) ) ;
#11929=CARTESIAN_POINT ( 'NONE',  ( 0.000000000000000000, 8.000000000000000000, 0.000000000000000000 ) ) ;
#11971=AXIS2_PLACEMENT_3D ( 'NONE', #19957, #983, #15355 ) ;
#11974=DIRECTION ( 'NONE',  ( -0.000000000000000000, -1.000000000000000000, -0.000000000000000000 ) ) ;
#11981=CARTESIAN_POINT ( 'NONE',  ( -31.81980515339462912, 11.00000000000000000, 31.81980515339465043 ) ) ;
#11982=CARTESIAN_POINT ( 'NONE',  ( -35.00000000000000000, 19.00000000000000000, -21.00000000000000000 ) ) ;
#12004=DIRECTION ( 'NONE',  ( 1.000000000000000000, 0.000000000000000000, 0.000000000000000000 ) ) ;
#12012=VECTOR ( 'NONE', #675, 1000.000000000000000 ) ;
#12014=DIRECTION ( 'NONE',  ( 0.000000000000000000, 0.000000000000000000, 1.000000000000000000 ) ) ;
#12018=AXIS2_PLACEMENT_3D ( 'NONE', #2507, #17039, #7257 ) ;
#12024=ORIENTED_EDGE ( 'NONE', *, *, #15113, .T. ) ;
#12034=DIRECTION ( 'NONE',  ( 1.000000000000000000, 0.000000000000000000, 0.000000000000000000 ) ) ;
#12062=AXIS2_PLACEMENT_3D ( 'NONE', #11131, #9796, #1847 ) ;
#12064=DIRECTION ( 'NONE',  ( -0.000000000000000000, -1.000000000000000000, -0.000000000000000000 ) ) ;
#12070=DIRECTION ( 'NONE',  ( 0.000000000000000000, 1.000000000000000000, -0.000000000000000000 ) ) ;
#12085=CARTESIAN_POINT ( 'NONE',  ( -31.81980515339462912, 8.000000000000000000, -35.11980515339465114 ) ) ;
#12094=AXIS2_PLACEMENT_3D ( 'NONE', #608, #5368, #8464 ) ;
#12104=ORIENTED_EDGE ( 'NONE', *, *, #15402, .T. ) ;
#12111=ORIENTED_EDGE ( 'NONE', *, *, #10506, .T. ) ;
#12136=ORIENTED_EDGE ( 'NONE', *, *, #19762, .T. ) ;
#12152=EDGE_CURVE ( 'NONE', #4285, #4676, #6731, .T. ) ;
#12172=CARTESIAN_POINT ( 'NONE',  ( -34.99999999999996447, 0.000000000000000000, -40.00000000000000711 ) ) ;
#12178=CARTESIAN_POINT ( 'NONE',  ( 21.00000000000000000, 19.00000000000000000, -31.00000000000003908 ) ) ;
#12193=VECTOR ( 'NONE', #14863, 1000.000000000000000 ) ;
#12197=PLANE ( 'NONE',  #11888 ) ;
#12215=CARTESIAN_POINT ( 'NONE',  ( 21.00000000000000000, 8.000000000000000000, -35.00000000000000711 ) ) ;
#12235=ORIENTED_EDGE ( 'NONE', *, *, #7113, .F. ) ;
#12246=AXIS2_PLACEMENT_3D ( 'NONE', #17796, #874, #3893 ) ;
#12248=DIRECTION ( 'NONE',  ( -0.000000000000000000, -0.000000000000000000, 1.000000000000000000 ) ) ;
#12282=EDGE_CURVE ( 'NONE', #13880, #3979, #8521, .T. ) ;
#12287=ORIENTED_EDGE ( 'NONE', *, *, #17099, .T. ) ;
#12300=DIRECTION ( 'NONE',  ( 0.000000000000000000, 0.000000000000000000, 1.000000000000000000 ) ) ;
#12311=AXIS2_PLACEMENT_3D ( 'NONE', #15649, #6256, #1576 ) ;
#12337=AXIS2_PLACEMENT_3D ( 'NONE', #4104, #5853, #10478 ) ;
#12341=DIRECTION ( 'NONE',  ( -1.000000000000000000, -0.000000000000000000, -0.000000000000000000 ) ) ;
#12345=CIRCLE ( 'NONE', #1793, 5.000000000000000888 ) ;
#12350=VECTOR ( 'NONE', #7923, 1000.000000000000000 ) ;
#12376=ORIENTED_EDGE ( 'NONE', *, *, #14322, .T. ) ;
#12392=EDGE_LOOP ( 'NONE', ( #3230, #10509, #14483, #1412 ) ) ;
#12393=DIRECTION ( 'NONE',  ( 1.000000000000000000, 0.000000000000000000, 0.000000000000000000 ) ) ;
#12401=EDGE_CURVE ( 'NONE', #53, #17182, #18395, .T. ) ;
#12403=VERTEX_POINT ( 'NONE', #10270 ) ;
#12406=CIRCLE ( 'NONE', #16052, 18.50000000000000000 ) ;
#12407=ORIENTED_EDGE ( 'NONE', *, *, #13913, .T. ) ;
#12440=LINE ( 'NONE', #13683, #6027 ) ;
#12454=DIRECTION ( 'NONE',  ( 0.000000000000000000, 1.000000000000000000, 0.000000000000000000 ) ) ;
#12471=AXIS2_PLACEMENT_3D ( 'NONE', #16433, #9929, #3943 ) ;
#12501=LINE ( 'NONE', #17130, #14976 ) ;
#12506=ORIENTED_EDGE ( 'NONE', *, *, #9260, .T. ) ;
#12507=DIRECTION ( 'NONE',  ( 0.000000000000000000, 1.000000000000000000, 0.000000000000000000 ) ) ;
#12512=EDGE_CURVE ( 'NONE', #13880, #9081, #20206, .T. ) ;
#12529=CYLINDRICAL_SURFACE ( 'NONE', #14569, 3.300000000000000711 ) ;
#12530=DIRECTION ( 'NONE',  ( -0.000000000000000000, -1.000000000000000000, -0.000000000000000000 ) ) ;
#12559=DIRECTION ( 'NONE',  ( 0.000000000000000000, 0.000000000000000000, 1.000000000000000000 ) ) ;
#12576=CARTESIAN_POINT ( 'NONE',  ( 31.81980515339464333, 0.000000000000000000, -31.81980515339463622 ) ) ;
#12584=DIRECTION ( 'NONE',  ( 1.000000000000000000, 0.000000000000000000, -0.000000000000000000 ) ) ;
#12588=ORIENTED_EDGE ( 'NONE', *, *, #15189, .F. ) ;
#12591=VERTEX_POINT ( 'NONE', #19409 ) ;
#12613=VERTEX_POINT ( 'NONE', #356 ) ;
#12639=VECTOR ( 'NONE', #4738, 1000.000000000000000 ) ;
#12652=EDGE_LOOP ( 'NONE', ( #1462, #14685, #14820, #1555, #11602, #12111 ) ) ;
#12657=EDGE_LOOP ( 'NONE', ( #4635, #6173, #19239, #414, #3488, #550, #18769, #665 ) ) ;
#12660=VECTOR ( 'NONE', #19291, 1000.000000000000000 ) ;
#12661=VERTEX_POINT ( 'NONE', #19803 ) ;
#12662=CARTESIAN_POINT ( 'NONE',  ( 31.81980515339464333, 11.00000000000000000, -35.11980515339463693 ) ) ;
#12672=LINE ( 'NONE', #16186, #6859 ) ;
#12682=ORIENTED_EDGE ( 'NONE', *, *, #585, .F. ) ;
#12687=VECTOR ( 'NONE', #20256, 1000.000000000000000 ) ;
#12692=CARTESIAN_POINT ( 'NONE',  ( -40.00000000000000000, 19.00000000000000000, 25.99999999999999645 ) ) ;
#12699=DIRECTION ( 'NONE',  ( 0.000000000000000000, 0.000000000000000000, 1.000000000000000000 ) ) ;
#12700=DIRECTION ( 'NONE',  ( 0.000000000000000000, -1.000000000000000000, 0.000000000000000000 ) ) ;
#12711=CIRCLE ( 'NONE', #14346, 3.300000000000000711 ) ;
#12716=CARTESIAN_POINT ( 'NONE',  ( 31.81980515339464333, 0.000000000000000000, 31.81980515339463622 ) ) ;
#12721=CARTESIAN_POINT ( 'NONE',  ( 21.00000000000000000, 19.00000000000000000, 35.00000000000001421 ) ) ;
#12728=CARTESIAN_POINT ( 'NONE',  ( -20.99999999999999645, 19.00000000000000000, -31.00000000000003908 ) ) ;
#12740=VECTOR ( 'NONE', #9568, 1000.000000000000000 ) ;
#12742=ORIENTED_EDGE ( 'NONE', *, *, #16318, .F. ) ;
#12749=CARTESIAN_POINT ( 'NONE',  ( 31.00000000000000000, 19.00000000000000000, 30.99999999999999289 ) ) ;
#12768=DIRECTION ( 'NONE',  ( -0.000000000000000000, -1.000000000000000000, -0.000000000000000000 ) ) ;
#12771=CARTESIAN_POINT ( 'NONE',  ( 0.000000000000000000, -3.000000000000000000, -18.50000000000000000 ) ) ;
#12779=CARTESIAN_POINT ( 'NONE',  ( -39.99999999999999289, 11.00000000000000000, 34.99999999999997868 ) ) ;
#12786=ADVANCED_FACE ( 'NONE', ( #10961 ), #18877, .T. ) ;
#12803=CARTESIAN_POINT ( 'NONE',  ( 31.81980515339464333, 0.000000000000000000, 35.11980515339463693 ) ) ;
#12812=LINE ( 'NONE', #4976, #6614 ) ;
#12815=DIRECTION ( 'NONE',  ( 0.000000000000000000, 0.000000000000000000, 1.000000000000000000 ) ) ;
#12817=AXIS2_PLACEMENT_3D ( 'NONE', #8883, #15173, #8982 ) ;
#12818=AXIS2_PLACEMENT_3D ( 'NONE', #12749, #17678, #20345 ) ;
#12828=PRODUCT_CONTEXT ( 'NONE', #366, 'mechanical' ) ;
#12830=DIRECTION ( 'NONE',  ( -0.000000000000000000, 1.000000000000000000, -0.000000000000000000 ) ) ;
#12847=FACE_OUTER_BOUND ( 'NONE', #14234, .T. ) ;
#12852=ORIENTED_EDGE ( 'NONE', *, *, #10292, .T. ) ;
#12862=ORIENTED_EDGE ( 'NONE', *, *, #9042, .T. ) ;
#12892=ORIENTED_EDGE ( 'NONE', *, *, #13557, .T. ) ;
#12895=DIRECTION ( 'NONE',  ( 0.000000000000000000, 0.000000000000000000, 1.000000000000000000 ) ) ;
#12898=LINE ( 'NONE', #7937, #9675 ) ;
#12901=FACE_OUTER_BOUND ( 'NONE', #13383, .T. ) ;
#12904=EDGE_CURVE ( 'NONE', #5141, #1964, #9199, .T. ) ;
#12917=VERTEX_POINT ( 'NONE', #9725 ) ;
#12940=AXIS2_PLACEMENT_3D ( 'NONE', #10581, #16694, #16781 ) ;
#12947=EDGE_LOOP ( 'NONE', ( #19472, #18483 ) ) ;
#12949=DIRECTION ( 'NONE',  ( -0.000000000000000000, -1.000000000000000000, -0.000000000000000000 ) ) ;
#12954=ORIENTED_EDGE ( 'NONE', *, *, #3605, .F. ) ;
#12959=CYLINDRICAL_SURFACE ( 'NONE', #12818, 9.999999999999998224 ) ;
#12979=EDGE_LOOP ( 'NONE', ( #7878, #7951, #12954, #14749 ) ) ;
#12986=AXIS2_PLACEMENT_3D ( 'NONE', #9419, #15729, #4990 ) ;
#13023=VECTOR ( 'NONE', #10281, 1000.000000000000000 ) ;
#13034=DIRECTION ( 'NONE',  ( -1.000000000000000000, -0.000000000000000000, -0.000000000000000000 ) ) ;
#13037=ORIENTED_EDGE ( 'NONE', *, *, #781, .F. ) ;
#13038=PLANE ( 'NONE',  #10390 ) ;
#13049=CARTESIAN_POINT ( 'NONE',  ( -26.00000000000000000, 19.00000000000000000, 40.00000000000001421 ) ) ;
#13052=DIRECTION ( 'NONE',  ( -0.000000000000000000, -1.000000000000000000, -0.000000000000000000 ) ) ;
#13058=VERTEX_POINT ( 'NONE', #7246 ) ;
#13062=ORIENTED_EDGE ( 'NONE', *, *, #17411, .T. ) ;
#13064=DIRECTION ( 'NONE',  ( -0.000000000000000000, -1.000000000000000000, -0.000000000000000000 ) ) ;
#13068=ADVANCED_FACE ( 'NONE', ( #19782 ), #16529, .T. ) ;
#13101=( NAMED_UNIT ( * ) PLANE_ANGLE_UNIT ( ) SI_UNIT ( $, .RADIAN. ) );
#13103=CARTESIAN_POINT ( 'NONE',  ( 31.81980515339464333, 0.000000000000000000, -31.81980515339463622 ) ) ;
#13110=VERTEX_POINT ( 'NONE', #2180 ) ;
#13124=ORIENTED_EDGE ( 'NONE', *, *, #7030, .T. ) ;
#13125=CIRCLE ( 'NONE', #2881, 35.00000000000000711 ) ;
#13133=EDGE_CURVE ( 'NONE', #3979, #9984, #8481, .T. ) ;
#13139=ORIENTED_EDGE ( 'NONE', *, *, #9260, .F. ) ;
#13145=EDGE_CURVE ( 'NONE', #6497, #12403, #16430, .T. ) ;
#13153=SURFACE_STYLE_USAGE ( .BOTH. , #6776 ) ;
#13161=LINE ( 'NONE', #5321, #18167 ) ;
#13165=VERTEX_POINT ( 'NONE', #15993 ) ;
#13173=CARTESIAN_POINT ( 'NONE',  ( 0.000000000000000000, 19.00100000000000122, -18.50000000000000000 ) ) ;
#13176=VECTOR ( 'NONE', #3999, 1000.000000000000000 ) ;
#13177=ORIENTED_EDGE ( 'NONE', *, *, #18561, .F. ) ;
#13188=SHAPE_REPRESENTATION_RELATIONSHIP ( 'NONE' , 'NONE' ,  #16597, #14042 ) ;
#13190=FACE_OUTER_BOUND ( 'NONE', #12657, .T. ) ;
#13206=CARTESIAN_POINT ( 'NONE',  ( -31.00000000000000000, 19.00000000000000000, -31.00000000000000000 ) ) ;
#13241=DIRECTION ( 'NONE',  ( -0.000000000000000000, -1.000000000000000000, -0.000000000000000000 ) ) ;
#13246=SURFACE_STYLE_FILL_AREA ( #17869 ) ;
#13265=EDGE_LOOP ( 'NONE', ( #2181, #1052 ) ) ;
#13268=VECTOR ( 'NONE', #2789, 1000.000000000000000 ) ;
#13271=ORIENTED_EDGE ( 'NONE', *, *, #308, .T. ) ;
#13278=CARTESIAN_POINT ( 'NONE',  ( 0.000000000000000000, -3.000000000000000000, 0.000000000000000000 ) ) ;
#13288=ORIENTED_EDGE ( 'NONE', *, *, #12512, .F. ) ;
#13304=DIRECTION ( 'NONE',  ( -1.000000000000000000, 0.000000000000000000, 3.854941057726251409E-16 ) ) ;
#13346=ORIENTED_EDGE ( 'NONE', *, *, #10250, .T. ) ;
#13355=AXIS2_PLACEMENT_3D ( 'NONE', #728, #19480, #18257 ) ;
#13379=AXIS2_PLACEMENT_3D ( 'NONE', #396, #19044, #14219 ) ;
#13383=EDGE_LOOP ( 'NONE', ( #10817, #13062, #15531, #8604 ) ) ;
#13385=CARTESIAN_POINT ( 'NONE',  ( 31.00000000000003553, 19.00000000000000000, 25.99999999999999645 ) ) ;
#13395=DIRECTION ( 'NONE',  ( -1.000000000000000000, 0.000000000000000000, 0.000000000000000000 ) ) ;
#13414=CARTESIAN_POINT ( 'NONE',  ( 31.00000000000000000, 8.000000000000000000, -21.00000000000000355 ) ) ;
#13416=CARTESIAN_POINT ( 'NONE',  ( -26.00000000000000000, 11.00000000000000000, -31.00000000000003908 ) ) ;
#13417=CARTESIAN_POINT ( 'NONE',  ( -35.00000000000000000, 8.000000000000000000, 20.99999999999999289 ) ) ;
#13438=LINE ( 'NONE', #10434, #3047 ) ;
#13446=VECTOR ( 'NONE', #18397, 1000.000000000000000 ) ;
#13449=ORIENTED_EDGE ( 'NONE', *, *, #1340, .F. ) ;
#13467=EDGE_CURVE ( 'NONE', #18235, #19590, #3695, .T. ) ;
#13472=ADVANCED_FACE ( 'NONE', ( #2134, #19533, #6905, #13190, #5343, #2440 ), #19839, .T. ) ;
#13473=VERTEX_POINT ( 'NONE', #5854 ) ;
#13488=DIRECTION ( 'NONE',  ( 0.000000000000000000, 0.000000000000000000, 1.000000000000000000 ) ) ;
#13497=CARTESIAN_POINT ( 'NONE',  ( 31.81980515339464333, 8.000000000000000000, 28.51980515339463906 ) ) ;
#13503=CARTESIAN_POINT ( 'NONE',  ( -39.99999999999999289, 11.00000000000000000, -26.00000000000000355 ) ) ;
#13536=VERTEX_POINT ( 'NONE', #4819 ) ;
#13557=EDGE_CURVE ( 'NONE', #3628, #8580, #4050, .T. ) ;
#13560=ORIENTED_EDGE ( 'NONE', *, *, #14045, .F. ) ;
#13589=VERTEX_POINT ( 'NONE', #9137 ) ;
#13626=FACE_OUTER_BOUND ( 'NONE', #3289, .T. ) ;
#13640=DIRECTION ( 'NONE',  ( -0.000000000000000000, -1.000000000000000000, -0.000000000000000000 ) ) ;
#13655=FACE_OUTER_BOUND ( 'NONE', #9475, .T. ) ;
#13670=DIRECTION ( 'NONE',  ( 0.000000000000000000, 0.000000000000000000, -1.000000000000000000 ) ) ;
#13677=FACE_OUTER_BOUND ( 'NONE', #3653, .T. ) ;
#13682=CARTESIAN_POINT ( 'NONE',  ( -26.00000000000000000, 19.00000000000000000, -31.00000000000003908 ) ) ;
#13683=CARTESIAN_POINT ( 'NONE',  ( 40.00000000000000711, 19.00000000000000000, -26.00000000000000355 ) ) ;
#13704=AXIS2_PLACEMENT_3D ( 'NONE', #1617, #6606, #12895 ) ;
#13706=LINE ( 'NONE', #15675, #1102 ) ;
#13719=VERTEX_POINT ( 'NONE', #9642 ) ;
#13733=DIRECTION ( 'NONE',  ( 0.000000000000000000, 0.000000000000000000, 1.000000000000000000 ) ) ;
#13738=DIRECTION ( 'NONE',  ( 0.000000000000000000, 1.000000000000000000, 0.000000000000000000 ) ) ;
#13741=LINE ( 'NONE', #13837, #9674 ) ;
#13745=DIRECTION ( 'NONE',  ( -0.000000000000000000, -1.000000000000000000, -0.000000000000000000 ) ) ;
#13750=FACE_BOUND ( 'NONE', #7995, .T. ) ;
#13792=CARTESIAN_POINT ( 'NONE',  ( 35.00000000000000711, 0.000000000000000000, -35.00000000000000711 ) ) ;
#13795=CARTESIAN_POINT ( 'NONE',  ( -31.00000000000000000, 11.00000000000000000, 25.99999999999999645 ) ) ;
#13837=CARTESIAN_POINT ( 'NONE',  ( -26.00000000000000000, 19.00000000000000000, -40.00000000000000711 ) ) ;
#13852=ORIENTED_EDGE ( 'NONE', *, *, #18776, .T. ) ;
#13869=CARTESIAN_POINT ( 'NONE',  ( 2.265596578422603396E-15, -3.000000000000000000, 18.50000000000000000 ) ) ;
#13880=VERTEX_POINT ( 'NONE', #19585 ) ;
#13893=LINE ( 'NONE', #5970, #3418 ) ;
#13899=EDGE_CURVE ( 'NONE', #13165, #4285, #8678, .T. ) ;
#13900=EDGE_CURVE ( 'NONE', #17522, #2504, #7240, .T. ) ;
#13904=ORIENTED_EDGE ( 'NONE', *, *, #18776, .F. ) ;
#13913=EDGE_CURVE ( 'NONE', #18235, #19815, #15251, .T. ) ;
#13922=ADVANCED_FACE ( 'NONE', ( #8788 ), #4159, .T. ) ;
#13923=FACE_OUTER_BOUND ( 'NONE', #12652, .T. ) ;
#13932=AXIS2_PLACEMENT_3D ( 'NONE', #11981, #19671, #7336 ) ;
#13942=PLANE ( 'NONE',  #5790 ) ;
#13973=CARTESIAN_POINT ( 'NONE',  ( -26.00000000000000000, 19.00000000000000000, 40.00000000000001421 ) ) ;
#13987=LINE ( 'NONE', #7897, #20242 ) ;
#13992=EDGE_LOOP ( 'NONE', ( #11289, #6375 ) ) ;
#13994=VECTOR ( 'NONE', #6155, 1000.000000000000000 ) ;
#13998=CARTESIAN_POINT ( 'NONE',  ( -39.99999999999999289, 11.00000000000000000, -26.00000000000000355 ) ) ;
#14007=DIRECTION ( 'NONE',  ( 0.000000000000000000, 0.000000000000000000, 1.000000000000000000 ) ) ;
#14039=EDGE_LOOP ( 'NONE', ( #15416, #4083, #4077, #17958 ) ) ;
#14042=ADVANCED_BREP_SHAPE_REPRESENTATION ( '', ( #1227, #2741 ), #14554 ) ;
#14045=EDGE_CURVE ( 'NONE', #14156, #9509, #5708, .T. ) ;
#14066=ORIENTED_EDGE ( 'NONE', *, *, #13145, .T. ) ;
#14074=CYLINDRICAL_SURFACE ( 'NONE', #5135, 18.50000000000000000 ) ;
#14116=CYLINDRICAL_SURFACE ( 'NONE', #12062, 3.299999999999997158 ) ;
#14120=FACE_BOUND ( 'NONE', #12947, .T. ) ;
#14124=EDGE_LOOP ( 'NONE', ( #10140, #844, #16769, #13139 ) ) ;
#14130=AXIS2_PLACEMENT_3D ( 'NONE', #6171, #1692, #8005 ) ;
#14149=AXIS2_PLACEMENT_3D ( 'NONE', #10142, #16442, #8583 ) ;
#14156=VERTEX_POINT ( 'NONE', #9897 ) ;
#14157=LINE ( 'NONE', #4892, #14676 ) ;
#14175=EDGE_CURVE ( 'NONE', #5141, #16598, #15262, .T. ) ;
#14207=CARTESIAN_POINT ( 'NONE',  ( -20.99999999999999645, 19.00000000000000000, 35.00000000000001421 ) ) ;
#14219=DIRECTION ( 'NONE',  ( 0.000000000000000000, 0.000000000000000000, -1.000000000000000000 ) ) ;
#14227=DIRECTION ( 'NONE',  ( -0.000000000000000000, -0.000000000000000000, 1.000000000000000000 ) ) ;
#14234=EDGE_LOOP ( 'NONE', ( #17251, #12104, #4333, #3538 ) ) ;
#14269=DIRECTION ( 'NONE',  ( -0.000000000000000000, -1.000000000000000000, -0.000000000000000000 ) ) ;
#14282=EDGE_CURVE ( 'NONE', #3192, #15503, #18020, .T. ) ;
#14310=DIRECTION ( 'NONE',  ( 0.000000000000000000, 0.000000000000000000, 1.000000000000000000 ) ) ;
#14314=EDGE_LOOP ( 'NONE', ( #10795, #15443, #16702, #15981 ) ) ;
#14322=EDGE_CURVE ( 'NONE', #7143, #9862, #19560, .T. ) ;
#14335=DIRECTION ( 'NONE',  ( -0.000000000000000000, -1.000000000000000000, -0.000000000000000000 ) ) ;
#14346=AXIS2_PLACEMENT_3D ( 'NONE', #19491, #16814, #2575 ) ;
#14347=VERTEX_POINT ( 'NONE', #13414 ) ;
#14358=DIRECTION ( 'NONE',  ( -1.000000000000000000, -0.000000000000000000, -0.000000000000000000 ) ) ;
#14379=DIRECTION ( 'NONE',  ( -0.000000000000000000, -1.000000000000000000, 0.000000000000000000 ) ) ;
#14422=ORIENTED_EDGE ( 'NONE', *, *, #11842, .T. ) ;
#14428=LINE ( 'NONE', #8046, #14682 ) ;
#14446=CARTESIAN_POINT ( 'NONE',  ( -39.99999999999999289, 11.00000000000000000, -34.99999999999997868 ) ) ;
#14460=ADVANCED_FACE ( 'NONE', ( #12847 ), #14074, .F. ) ;
#14465=EDGE_LOOP ( 'NONE', ( #17205, #18205, #8781, #7564 ) ) ;
#14476=( LENGTH_UNIT ( ) NAMED_UNIT ( * ) SI_UNIT ( .MILLI., .METRE. ) );
#14483=ORIENTED_EDGE ( 'NONE', *, *, #10250, .F. ) ;
#14486=ORIENTED_EDGE ( 'NONE', *, *, #16313, .T. ) ;
#14491=CIRCLE ( 'NONE', #16483, 10.00000000000000178 ) ;
#14497=LINE ( 'NONE', #16277, #4442 ) ;
#14510=CARTESIAN_POINT ( 'NONE',  ( -34.99999999999996447, 11.00000000000000000, 40.00000000000000711 ) ) ;
#14525=PLANE ( 'NONE',  #17309 ) ;
#14536=EDGE_CURVE ( 'NONE', #715, #6120, #3127, .T. ) ;
#14545=DIRECTION ( 'NONE',  ( -1.000000000000000000, 0.000000000000000000, -0.000000000000000000 ) ) ;
#14554=( GEOMETRIC_REPRESENTATION_CONTEXT ( 3 ) GLOBAL_UNCERTAINTY_ASSIGNED_CONTEXT ( ( #19541 ) ) GLOBAL_UNIT_ASSIGNED_CONTEXT ( ( #5342, #13101, #17902 ) ) REPRESENTATION_CONTEXT ( 'NONE', 'WORKASPACE' ) );
#14555=EDGE_CURVE ( 'NONE', #18007, #53, #14779, .T. ) ;
#14569=AXIS2_PLACEMENT_3D ( 'NONE', #18702, #3034, #3251 ) ;
#14572=CARTESIAN_POINT ( 'NONE',  ( 35.00000000000000711, 8.000000000000000000, -35.00000000000000711 ) ) ;
#14576=DIRECTION ( 'NONE',  ( 0.000000000000000000, 0.000000000000000000, -1.000000000000000000 ) ) ;
#14578=LINE ( 'NONE', #11982, #10611 ) ;
#14595=AXIS2_PLACEMENT_3D ( 'NONE', #7018, #13304, #14735 ) ;
#14599=DIRECTION ( 'NONE',  ( 0.000000000000000000, -1.000000000000000000, 0.000000000000000000 ) ) ;
#14610=DIRECTION ( 'NONE',  ( 0.000000000000000000, 0.000000000000000000, -1.000000000000000000 ) ) ;
#14619=VERTEX_POINT ( 'NONE', #15508 ) ;
#14625=VERTEX_POINT ( 'NONE', #8808 ) ;
#14633=LINE ( 'NONE', #17718, #774 ) ;
#14635=PLANE ( 'NONE',  #14595 ) ;
#14638=CARTESIAN_POINT ( 'NONE',  ( 31.00000000000003553, 19.00000000000000000, 20.99999999999999289 ) ) ;
#14670=LINE ( 'NONE', #8566, #12193 ) ;
#14676=VECTOR ( 'NONE', #9322, 1000.000000000000000 ) ;
#14679=ORIENTED_EDGE ( 'NONE', *, *, #1577, .F. ) ;
#14682=VECTOR ( 'NONE', #14335, 1000.000000000000000 ) ;
#14685=ORIENTED_EDGE ( 'NONE', *, *, #13133, .T. ) ;
#14693=CARTESIAN_POINT ( 'NONE',  ( 0.000000000000000000, 8.000000000000000000, 0.000000000000000000 ) ) ;
#14703=CIRCLE ( 'NONE', #2505, 10.00000000000000178 ) ;
#14705=DIRECTION ( 'NONE',  ( 0.000000000000000000, 0.000000000000000000, -1.000000000000000000 ) ) ;
#14707=ORIENTED_EDGE ( 'NONE', *, *, #1162, .T. ) ;
#14709=DIRECTION ( 'NONE',  ( -0.000000000000000000, -1.000000000000000000, -0.000000000000000000 ) ) ;
#14729=ORIENTED_EDGE ( 'NONE', *, *, #914, .T. ) ;
#14732=DIRECTION ( 'NONE',  ( -0.000000000000000000, 1.000000000000000000, -0.000000000000000000 ) ) ;
#14735=DIRECTION ( 'NONE',  ( 3.854941057726251409E-16, 0.000000000000000000, 1.000000000000000000 ) ) ;
#14740=CARTESIAN_POINT ( 'NONE',  ( 31.00000000000000000, 19.00000000000000000, -21.00000000000000355 ) ) ;
#14749=ORIENTED_EDGE ( 'NONE', *, *, #17667, .F. ) ;
#14751=CARTESIAN_POINT ( 'NONE',  ( -20.99999999999999645, 19.00000000000000000, 35.00000000000001421 ) ) ;
#14754=EDGE_CURVE ( 'NONE', #13719, #6685, #122, .T. ) ;
#14763=CARTESIAN_POINT ( 'NONE',  ( 40.00000000000000711, 19.00000000000000000, -26.00000000000000355 ) ) ;
#14764=CYLINDRICAL_SURFACE ( 'NONE', #19215, 18.50000000000000000 ) ;
#14779=LINE ( 'NONE', #17771, #1123 ) ;
#14807=FACE_OUTER_BOUND ( 'NONE', #19442, .T. ) ;
#14812=CARTESIAN_POINT ( 'NONE',  ( -31.81980515339462912, 8.000000000000000000, 28.51980515339464972 ) ) ;
#14820=ORIENTED_EDGE ( 'NONE', *, *, #17336, .T. ) ;
#14843=ORIENTED_EDGE ( 'NONE', *, *, #13900, .T. ) ;
#14863=DIRECTION ( 'NONE',  ( -0.000000000000000000, -1.000000000000000000, -0.000000000000000000 ) ) ;
#14869=FACE_OUTER_BOUND ( 'NONE', #10987, .T. ) ;
#14877=UNCERTAINTY_MEASURE_WITH_UNIT (LENGTH_MEASURE( 1.000000000000000082E-05 ), #14476, 'distance_accuracy_value', 'NONE');
#14878=EDGE_LOOP ( 'NONE', ( #20338, #10203, #2896, #9382, #17714, #3410 ) ) ;
#14898=VERTEX_POINT ( 'NONE', #2585 ) ;
#14907=CARTESIAN_POINT ( 'NONE',  ( 21.00000000000000000, 8.000000000000000000, -31.00000000000003908 ) ) ;
#14918=CLOSED_SHELL ( 'NONE', ( #14460, #9410, #3334, #19831, #20267, #17419, #13472, #10226, #18365, #13068, #16831, #5242, #3130, #2683, #19092, #7903, #5787, #2566, #18727, #4736, #7850, #2261, #2549, #15286, #2670, #16593, #16435, #8562, #16703, #6208, #3190, #1154, #6383, #15006, #8391, #11103, #4323, #10359, #10512, #18063, #10971, #2198, #10018, #13922, #12786, #15735, #9660, #16990, #18939, #6895, #11812, #19177, #11538, #15056, #15357, #4961 ) ) ;
#14952=FACE_BOUND ( 'NONE', #13992, .T. ) ;
#14954=CIRCLE ( 'NONE', #15287, 4.999999999999997335 ) ;
#14955=CARTESIAN_POINT ( 'NONE',  ( 31.81980515339464333, 0.000000000000000000, -28.51980515339463906 ) ) ;
#14958=EDGE_LOOP ( 'NONE', ( #146, #15390, #13177, #2416, #14729, #8602, #2649, #14486 ) ) ;
#14960=ORIENTED_EDGE ( 'NONE', *, *, #10288, .T. ) ;
#14976=VECTOR ( 'NONE', #6529, 1000.000000000000000 ) ;
#14990=ORIENTED_EDGE ( 'NONE', *, *, #10891, .F. ) ;
#14992=AXIS2_PLACEMENT_3D ( 'NONE', #14693, #11589, #18062 ) ;
#14995=CARTESIAN_POINT ( 'NONE',  ( 35.00000000000000711, 11.00000000000000000, 35.00000000000000711 ) ) ;
#15006=ADVANCED_FACE ( 'NONE', ( #15382 ), #840, .T. ) ;
#15011=VECTOR ( 'NONE', #304, 1000.000000000000000 ) ;
#15014=ORIENTED_EDGE ( 'NONE', *, *, #17099, .F. ) ;
#15020=PLANE ( 'NONE',  #12246 ) ;
#15024=FACE_OUTER_BOUND ( 'NONE', #14465, .T. ) ;
#15025=CARTESIAN_POINT ( 'NONE',  ( -39.99999999999999289, 11.00000000000000000, 25.99999999999999645 ) ) ;
#15051=PLANE ( 'NONE',  #8576 ) ;
#15052=CARTESIAN_POINT ( 'NONE',  ( 26.00000000000000000, 19.00000000000000000, 40.00000000000001421 ) ) ;
#15056=ADVANCED_FACE ( 'NONE', ( #13923, #14120 ), #17508, .T. ) ;
#15069=DIRECTION ( 'NONE',  ( 0.000000000000000000, 0.000000000000000000, 1.000000000000000000 ) ) ;
#15073=DIRECTION ( 'NONE',  ( 0.000000000000000000, 1.000000000000000000, 0.000000000000000000 ) ) ;
#15113=EDGE_CURVE ( 'NONE', #10510, #15692, #20113, .T. ) ;
#15119=VECTOR ( 'NONE', #12393, 1000.000000000000000 ) ;
#15128=EDGE_LOOP ( 'NONE', ( #7629, #6677, #18983, #4089 ) ) ;
#15138=LINE ( 'NONE', #10190, #6612 ) ;
#15151=EDGE_LOOP ( 'NONE', ( #13271, #19293, #16351, #11373, #8821, #13346 ) ) ;
#15163=DIRECTION ( 'NONE',  ( -0.000000000000000000, -1.000000000000000000, -0.000000000000000000 ) ) ;
#15171=EDGE_CURVE ( 'NONE', #8912, #5141, #6435, .T. ) ;
#15172=EDGE_LOOP ( 'NONE', ( #20333, #5251, #7598, #13288 ) ) ;
#15173=DIRECTION ( 'NONE',  ( 0.000000000000000000, 1.000000000000000000, 0.000000000000000000 ) ) ;
#15182=ORIENTED_EDGE ( 'NONE', *, *, #20178, .F. ) ;
#15184=CARTESIAN_POINT ( 'NONE',  ( -31.00000000000000000, 8.000000000000000000, 30.99999999999999289 ) ) ;
#15189=EDGE_CURVE ( 'NONE', #6242, #12591, #10850, .T. ) ;
#15202=VECTOR ( 'NONE', #8506, 1000.000000000000000 ) ;
#15208=LINE ( 'NONE', #7575, #7112 ) ;
#15220=EDGE_CURVE ( 'NONE', #5238, #13110, #12501, .T. ) ;
#15251=CIRCLE ( 'NONE', #13932, 3.300000000000004263 ) ;
#15253=DIRECTION ( 'NONE',  ( -0.000000000000000000, -1.000000000000000000, -0.000000000000000000 ) ) ;
#15262=CIRCLE ( 'NONE', #6386, 10.00000000000000178 ) ;
#15263=CIRCLE ( 'NONE', #17226, 3.300000000000000711 ) ;
#15268=LINE ( 'NONE', #5682, #17925 ) ;
#15286=ADVANCED_FACE ( 'NONE', ( #11426 ), #589, .F. ) ;
#15287=AXIS2_PLACEMENT_3D ( 'NONE', #3612, #5169, #6823 ) ;
#15315=VECTOR ( 'NONE', #4782, 1000.000000000000000 ) ;
#15318=EDGE_CURVE ( 'NONE', #12661, #6513, #17705, .T. ) ;
#15328=DIRECTION ( 'NONE',  ( -0.000000000000000000, 1.000000000000000000, -0.000000000000000000 ) ) ;
#15330=CARTESIAN_POINT ( 'NONE',  ( -31.00000000000000000, 19.00000000000000000, 30.99999999999999289 ) ) ;
#15349=ORIENTED_EDGE ( 'NONE', *, *, #4220, .F. ) ;
#15355=DIRECTION ( 'NONE',  ( 0.000000000000000000, 0.000000000000000000, -1.000000000000000000 ) ) ;
#15357=ADVANCED_FACE ( 'NONE', ( #15992, #283 ), #881, .T. ) ;
#15382=FACE_OUTER_BOUND ( 'NONE', #18989, .T. ) ;
#15390=ORIENTED_EDGE ( 'NONE', *, *, #14555, .F. ) ;
#15392=EDGE_LOOP ( 'NONE', ( #17787, #19001, #9319, #11057 ) ) ;
#15396=CARTESIAN_POINT ( 'NONE',  ( 31.00000000000003553, 19.00000000000000000, 20.99999999999999289 ) ) ;
#15402=EDGE_CURVE ( 'NONE', #6120, #4513, #19730, .T. ) ;
#15415=EDGE_LOOP ( 'NONE', ( #4310, #12742, #13449, #17137, #12862, #2368, #5013, #16945 ) ) ;
#15416=ORIENTED_EDGE ( 'NONE', *, *, #14754, .T. ) ;
#15430=DIRECTION ( 'NONE',  ( 1.000000000000000000, 0.000000000000000000, 0.000000000000000000 ) ) ;
#15439=EDGE_CURVE ( 'NONE', #9081, #10510, #13987, .T. ) ;
#15443=ORIENTED_EDGE ( 'NONE', *, *, #15318, .F. ) ;
#15446=DIRECTION ( 'NONE',  ( 0.000000000000000000, 0.000000000000000000, 1.000000000000000000 ) ) ;
#15451=AXIS2_PLACEMENT_3D ( 'NONE', #17114, #6487, #1831 ) ;
#15458=CARTESIAN_POINT ( 'NONE',  ( 26.00000000000000000, 11.00000000000000000, 31.00000000000003197 ) ) ;
#15469=ORIENTED_EDGE ( 'NONE', *, *, #10744, .F. ) ;
#15476=CARTESIAN_POINT ( 'NONE',  ( -40.00000000000000000, 19.00000000000000000, 25.99999999999999645 ) ) ;
#15477=EDGE_CURVE ( 'NONE', #8912, #3482, #18618, .T. ) ;
#15484=AXIS2_PLACEMENT_3D ( 'NONE', #12716, #10953, #18969 ) ;
#15485=CARTESIAN_POINT ( 'NONE',  ( 0.000000000000000000, 0.000000000000000000, 35.00000000000000711 ) ) ;
#15486=DIRECTION ( 'NONE',  ( 0.000000000000000000, -0.000000000000000000, 1.000000000000000000 ) ) ;
#15490=DIRECTION ( 'NONE',  ( 0.000000000000000000, 0.000000000000000000, 1.000000000000000000 ) ) ;
#15501=CARTESIAN_POINT ( 'NONE',  ( 26.00000000000000355, 19.00000000000000000, -31.00000000000004263 ) ) ;
#15503=VERTEX_POINT ( 'NONE', #9338 ) ;
#15508=CARTESIAN_POINT ( 'NONE',  ( -31.81980515339462912, 0.000000000000000000, 35.11980515339465825 ) ) ;
#15515=VERTEX_POINT ( 'NONE', #4818 ) ;
#15519=EDGE_LOOP ( 'NONE', ( #5208, #5669, #17643, #1515 ) ) ;
#15531=ORIENTED_EDGE ( 'NONE', *, *, #585, .T. ) ;
#15538=CARTESIAN_POINT ( 'NONE',  ( 21.00000000000000000, 19.00000000000000000, 31.00000000000006395 ) ) ;
#15553=AXIS2_PLACEMENT_3D ( 'NONE', #6764, #13052, #19302 ) ;
#15577=EDGE_CURVE ( 'NONE', #5039, #14898, #5399, .T. ) ;
#15591=ORIENTED_EDGE ( 'NONE', *, *, #16220, .T. ) ;
#15600=CARTESIAN_POINT ( 'NONE',  ( 31.81980515339464333, 11.00000000000000000, 31.81980515339463622 ) ) ;
#15601=PLANE ( 'NONE',  #16610 ) ;
#15605=AXIS2_PLACEMENT_3D ( 'NONE', #9625, #17454, #15947 ) ;
#15612=DIRECTION ( 'NONE',  ( -1.000000000000000000, 0.000000000000000000, -0.000000000000000000 ) ) ;
#15649=CARTESIAN_POINT ( 'NONE',  ( 31.00000000000000000, 19.00000000000000000, 30.99999999999999289 ) ) ;
#15655=VECTOR ( 'NONE', #17800, 1000.000000000000000 ) ;
#15659=VECTOR ( 'NONE', #11556, 1000.000000000000000 ) ;
#15671=ORIENTED_EDGE ( 'NONE', *, *, #17986, .F. ) ;
#15675=CARTESIAN_POINT ( 'NONE',  ( -39.99999999999999289, 11.00000000000000000, 25.99999999999999645 ) ) ;
#15676=ORIENTED_EDGE ( 'NONE', *, *, #1411, .T. ) ;
#15692=VERTEX_POINT ( 'NONE', #14763 ) ;
#15702=LINE ( 'NONE', #16826, #412 ) ;
#15711=EDGE_CURVE ( 'NONE', #17040, #5279, #18453, .T. ) ;
#15722=DIRECTION ( 'NONE',  ( 0.000000000000000000, 0.000000000000000000, -1.000000000000000000 ) ) ;
#15723=CARTESIAN_POINT ( 'NONE',  ( 35.00000000000000711, 0.000000000000000000, 35.00000000000000711 ) ) ;
#15728=DIRECTION ( 'NONE',  ( 0.000000000000000000, 0.000000000000000000, -1.000000000000000000 ) ) ;
#15729=DIRECTION ( 'NONE',  ( -1.000000000000000000, 0.000000000000000000, 0.000000000000000000 ) ) ;
#15735=ADVANCED_FACE ( 'NONE', ( #13626 ), #15601, .T. ) ;
#15736=CARTESIAN_POINT ( 'NONE',  ( 31.00000000000003553, 19.00000000000000000, 25.99999999999999645 ) ) ;
#15738=ORIENTED_EDGE ( 'NONE', *, *, #17051, .F. ) ;
#15782=ORIENTED_EDGE ( 'NONE', *, *, #10292, .F. ) ;
#15786=FACE_OUTER_BOUND ( 'NONE', #14039, .T. ) ;
#15795=VECTOR ( 'NONE', #963, 1000.000000000000000 ) ;
#15840=DIRECTION ( 'NONE',  ( -0.000000000000000000, -0.000000000000000000, 1.000000000000000000 ) ) ;
#15841=AXIS2_PLACEMENT_3D ( 'NONE', #6640, #19387, #11571 ) ;
#15844=CARTESIAN_POINT ( 'NONE',  ( 31.81980515339464333, 8.000000000000000000, -35.11980515339463693 ) ) ;
#15889=AXIS2_PLACEMENT_3D ( 'NONE', #13278, #5444, #9225 ) ;
#15891=CARTESIAN_POINT ( 'NONE',  ( -40.00000000000000000, 19.00000000000000000, 25.99999999999999645 ) ) ;
#15918=LINE ( 'NONE', #28, #11788 ) ;
#15939=VERTEX_POINT ( 'NONE', #14955 ) ;
#15940=AXIS2_PLACEMENT_3D ( 'NONE', #11111, #1710, #12559 ) ;
#15947=DIRECTION ( 'NONE',  ( 0.000000000000000000, 0.000000000000000000, -1.000000000000000000 ) ) ;
#15973=CARTESIAN_POINT ( 'NONE',  ( -20.99999999999999645, 19.00000000000000000, 35.00000000000001421 ) ) ;
#15980=VECTOR ( 'NONE', #18571, 1000.000000000000000 ) ;
#15981=ORIENTED_EDGE ( 'NONE', *, *, #15220, .T. ) ;
#15984=CARTESIAN_POINT ( 'NONE',  ( -31.00000000000003553, 19.00000000000000000, 25.99999999999999645 ) ) ;
#15992=FACE_OUTER_BOUND ( 'NONE', #2875, .T. ) ;
#15993=CARTESIAN_POINT ( 'NONE',  ( -31.81980515339462912, 11.00000000000000000, -35.11980515339465114 ) ) ;
#15994=VECTOR ( 'NONE', #1814, 1000.000000000000000 ) ;
#16022=CARTESIAN_POINT ( 'NONE',  ( 0.000000000000000000, -3.000000000000000000, 0.000000000000000000 ) ) ;
#16035=DIRECTION ( 'NONE',  ( 0.000000000000000000, 1.000000000000000000, -0.000000000000000000 ) ) ;
#16049=VERTEX_POINT ( 'NONE', #2669 ) ;
#16051=ORIENTED_EDGE ( 'NONE', *, *, #10398, .F. ) ;
#16052=AXIS2_PLACEMENT_3D ( 'NONE', #16679, #14599, #480 ) ;
#16074=EDGE_CURVE ( 'NONE', #6242, #5571, #17012, .T. ) ;
#16104=CYLINDRICAL_SURFACE ( 'NONE', #13704, 35.00000000000000711 ) ;
#16108=LINE ( 'NONE', #3, #15011 ) ;
#16130=AXIS2_PLACEMENT_3D ( 'NONE', #13103, #9284, #19026 ) ;
#16146=ORIENTED_EDGE ( 'NONE', *, *, #4486, .F. ) ;
#16171=LINE ( 'NONE', #9956, #15202 ) ;
#16184=DIRECTION ( 'NONE',  ( 0.000000000000000000, 0.000000000000000000, 1.000000000000000000 ) ) ;
#16186=CARTESIAN_POINT ( 'NONE',  ( -35.00000000000000000, 8.000000000000000000, 20.99999999999999289 ) ) ;
#16203=DIRECTION ( 'NONE',  ( -0.000000000000000000, -1.000000000000000000, -0.000000000000000000 ) ) ;
#16219=EDGE_LOOP ( 'NONE', ( #4660, #4242, #10696, #1131 ) ) ;
#16220=EDGE_CURVE ( 'NONE', #17040, #16049, #19441, .T. ) ;
#16263=PLANE ( 'NONE',  #2570 ) ;
#16269=VERTEX_POINT ( 'NONE', #16696 ) ;
#16270=EDGE_LOOP ( 'NONE', ( #7536, #1578, #9167, #6491 ) ) ;
#16277=CARTESIAN_POINT ( 'NONE',  ( 40.00000000000000711, 19.00000000000000000, 25.99999999999999645 ) ) ;
#16280=VECTOR ( 'NONE', #10518, 1000.000000000000000 ) ;
#16294=CARTESIAN_POINT ( 'NONE',  ( -31.81980515339462912, 8.000000000000000000, -31.81980515339465043 ) ) ;
#16313=EDGE_CURVE ( 'NONE', #6685, #17182, #18095, .T. ) ;
#16318=EDGE_CURVE ( 'NONE', #17762, #14156, #18203, .T. ) ;
#16323=ORIENTED_EDGE ( 'NONE', *, *, #7097, .T. ) ;
#16325=CIRCLE ( 'NONE', #6725, 10.00000000000000178 ) ;
#16342=CYLINDRICAL_SURFACE ( 'NONE', #15841, 3.299999999999997158 ) ;
#16351=ORIENTED_EDGE ( 'NONE', *, *, #10744, .T. ) ;
#16353=ORIENTED_EDGE ( 'NONE', *, *, #4099, .F. ) ;
#16359=PRESENTATION_STYLE_ASSIGNMENT (( #13153 ) ) ;
#16377=ORIENTED_EDGE ( 'NONE', *, *, #4220, .T. ) ;
#16401=ORIENTED_EDGE ( 'NONE', *, *, #2312, .F. ) ;
#16430=LINE ( 'NONE', #2268, #12350 ) ;
#16433=CARTESIAN_POINT ( 'NONE',  ( -31.81980515339462912, 0.000000000000000000, 31.81980515339465043 ) ) ;
#16435=ADVANCED_FACE ( 'NONE', ( #169 ), #18714, .F. ) ;
#16441=DIRECTION ( 'NONE',  ( 0.000000000000000000, 0.000000000000000000, -1.000000000000000000 ) ) ;
#16442=DIRECTION ( 'NONE',  ( -0.000000000000000000, -1.000000000000000000, -0.000000000000000000 ) ) ;
#16444=EDGE_CURVE ( 'NONE', #14898, #3610, #7900, .T. ) ;
#16481=VERTEX_POINT ( 'NONE', #8425 ) ;
#16483=AXIS2_PLACEMENT_3D ( 'NONE', #7864, #20228, #6227 ) ;
#16529=CYLINDRICAL_SURFACE ( 'NONE', #13355, 4.999999999999997335 ) ;
#16538=DIRECTION ( 'NONE',  ( 1.000000000000000000, 0.000000000000000000, 0.000000000000000000 ) ) ;
#16565=EDGE_CURVE ( 'NONE', #10095, #3482, #18328, .T. ) ;
#16572=ORIENTED_EDGE ( 'NONE', *, *, #467, .F. ) ;
#16576=CARTESIAN_POINT ( 'NONE',  ( -20.99999999999999645, 19.00000000000000000, -31.00000000000003908 ) ) ;
#16593=ADVANCED_FACE ( 'NONE', ( #4232 ), #1399, .F. ) ;
#16597=SHAPE_REPRESENTATION ( 'Servo-Head', ( #2741 ), #14554 ) ;
#16598=VERTEX_POINT ( 'NONE', #4627 ) ;
#16610=AXIS2_PLACEMENT_3D ( 'NONE', #12178, #5693, #13733 ) ;
#16618=DIRECTION ( 'NONE',  ( -0.000000000000000000, -1.000000000000000000, -0.000000000000000000 ) ) ;
#16661=CARTESIAN_POINT ( 'NONE',  ( -31.81980515339462912, 11.00000000000000000, -28.51980515339464972 ) ) ;
#16667=DIRECTION ( 'NONE',  ( 0.000000000000000000, 1.000000000000000000, 0.000000000000000000 ) ) ;
#16679=CARTESIAN_POINT ( 'NONE',  ( 0.000000000000000000, -3.000000000000000000, 0.000000000000000000 ) ) ;
#16692=AXIS2_PLACEMENT_3D ( 'NONE', #9149, #15446, #1275 ) ;
#16694=DIRECTION ( 'NONE',  ( 0.000000000000000000, -1.000000000000000000, 0.000000000000000000 ) ) ;
#16696=CARTESIAN_POINT ( 'NONE',  ( 26.00000000000000355, 11.00000000000000000, -40.00000000000000711 ) ) ;
#16702=ORIENTED_EDGE ( 'NONE', *, *, #5878, .F. ) ;
#16703=ADVANCED_FACE ( 'NONE', ( #17091 ), #6082, .F. ) ;
#16727=LINE ( 'NONE', #11580, #16994 ) ;
#16730=CIRCLE ( 'NONE', #12094, 4.999999999999997335 ) ;
#16736=CARTESIAN_POINT ( 'NONE',  ( -35.00000000000000000, 19.00000000000000000, -21.00000000000000000 ) ) ;
#16761=FACE_OUTER_BOUND ( 'NONE', #2314, .T. ) ;
#16769=ORIENTED_EDGE ( 'NONE', *, *, #13899, .T. ) ;
#16772=CARTESIAN_POINT ( 'NONE',  ( 25.99999999999999645, 11.00000000000000000, 40.00000000000000711 ) ) ;
#16777=CIRCLE ( 'NONE', #16130, 3.299999999999997158 ) ;
#16781=DIRECTION ( 'NONE',  ( 0.000000000000000000, -0.000000000000000000, -1.000000000000000000 ) ) ;
#16785=ORIENTED_EDGE ( 'NONE', *, *, #19476, .T. ) ;
#16814=DIRECTION ( 'NONE',  ( 0.000000000000000000, 1.000000000000000000, 0.000000000000000000 ) ) ;
#16825=CARTESIAN_POINT ( 'NONE',  ( 31.00000000000006750, 19.00000000000000000, -21.00000000000000355 ) ) ;
#16826=CARTESIAN_POINT ( 'NONE',  ( -26.00000000000000000, 19.00000000000000000, -31.00000000000003908 ) ) ;
#16831=ADVANCED_FACE ( 'NONE', ( #16761 ), #12197, .F. ) ;
#16833=VECTOR ( 'NONE', #11473, 1000.000000000000000 ) ;
#16855=CARTESIAN_POINT ( 'NONE',  ( -26.00000000000000000, 11.00000000000000000, -40.00000000000000711 ) ) ;
#16857=ORIENTED_EDGE ( 'NONE', *, *, #10264, .F. ) ;
#16862=LINE ( 'NONE', #7384, #18607 ) ;
#16867=VERTEX_POINT ( 'NONE', #7567 ) ;
#16888=VECTOR ( 'NONE', #15163, 1000.000000000000000 ) ;
#16943=DIRECTION ( 'NONE',  ( 0.000000000000000000, 0.000000000000000000, 1.000000000000000000 ) ) ;
#16945=ORIENTED_EDGE ( 'NONE', *, *, #16444, .T. ) ;
#16954=ORIENTED_EDGE ( 'NONE', *, *, #10288, .F. ) ;
#16958=DIRECTION ( 'NONE',  ( 0.000000000000000000, -1.000000000000000000, 0.000000000000000000 ) ) ;
#16973=FACE_OUTER_BOUND ( 'NONE', #19716, .T. ) ;
#16974=VECTOR ( 'NONE', #9430, 1000.000000000000000 ) ;
#16984=DIRECTION ( 'NONE',  ( 0.000000000000000000, 0.000000000000000000, 1.000000000000000000 ) ) ;
#16990=ADVANCED_FACE ( 'NONE', ( #18118 ), #9930, .T. ) ;
#16994=VECTOR ( 'NONE', #13241, 1000.000000000000000 ) ;
#16998=FACE_OUTER_BOUND ( 'NONE', #1493, .T. ) ;
#17012=LINE ( 'NONE', #7435, #17260 ) ;
#17030=VERTEX_POINT ( 'NONE', #10304 ) ;
#17035=ORIENTED_EDGE ( 'NONE', *, *, #15711, .F. ) ;
#17039=DIRECTION ( 'NONE',  ( 1.000000000000000000, -0.000000000000000000, 0.000000000000000000 ) ) ;
#17040=VERTEX_POINT ( 'NONE', #13049 ) ;
#17051=EDGE_CURVE ( 'NONE', #5279, #9984, #11160, .T. ) ;
#17073=CARTESIAN_POINT ( 'NONE',  ( 0.000000000000000000, 0.000000000000000000, 0.000000000000000000 ) ) ;
#17080=EDGE_CURVE ( 'NONE', #1902, #6860, #18332, .T. ) ;
#17091=FACE_OUTER_BOUND ( 'NONE', #15172, .T. ) ;
#17092=LINE ( 'NONE', #13795, #7935 ) ;
#17099=EDGE_CURVE ( 'NONE', #5525, #18451, #17092, .T. ) ;
#17101=ORIENTED_EDGE ( 'NONE', *, *, #399, .T. ) ;
#17106=CARTESIAN_POINT ( 'NONE',  ( -31.00000000000000000, 19.00000000000000000, -31.00000000000000000 ) ) ;
#17114=CARTESIAN_POINT ( 'NONE',  ( -34.99999999999999289, 8.000000000000000000, 35.00000000000000711 ) ) ;
#17121=EDGE_CURVE ( 'NONE', #10263, #6022, #7919, .T. ) ;
#17130=CARTESIAN_POINT ( 'NONE',  ( -39.99999999999999289, 8.000000000000000000, 34.99999999999997868 ) ) ;
#17137=ORIENTED_EDGE ( 'NONE', *, *, #19476, .F. ) ;
#17152=DIRECTION ( 'NONE',  ( 0.000000000000000000, 0.000000000000000000, 1.000000000000000000 ) ) ;
#17166=DIRECTION ( 'NONE',  ( 0.000000000000000000, 0.000000000000000000, -1.000000000000000000 ) ) ;
#17175=CARTESIAN_POINT ( 'NONE',  ( 26.00000000000000000, 19.00000000000000000, 40.00000000000001421 ) ) ;
#17182=VERTEX_POINT ( 'NONE', #10503 ) ;
#17185=DIRECTION ( 'NONE',  ( 0.000000000000000000, 1.000000000000000000, 0.000000000000000000 ) ) ;
#17201=ORIENTED_EDGE ( 'NONE', *, *, #2053, .T. ) ;
#17205=ORIENTED_EDGE ( 'NONE', *, *, #5949, .F. ) ;
#17217=CARTESIAN_POINT ( 'NONE',  ( -26.00000000000000000, 11.00000000000000000, -31.00000000000003908 ) ) ;
#17226=AXIS2_PLACEMENT_3D ( 'NONE', #18168, #16667, #12300 ) ;
#17251=ORIENTED_EDGE ( 'NONE', *, *, #14536, .T. ) ;
#17254=CIRCLE ( 'NONE', #18230, 4.999999999999997335 ) ;
#17258=VECTOR ( 'NONE', #6014, 1000.000000000000000 ) ;
#17260=VECTOR ( 'NONE', #16618, 1000.000000000000000 ) ;
#17277=CARTESIAN_POINT ( 'NONE',  ( -35.00000000000000000, 19.00000000000000000, 20.99999999999999289 ) ) ;
#17289=ORIENTED_EDGE ( 'NONE', *, *, #7030, .F. ) ;
#17309=AXIS2_PLACEMENT_3D ( 'NONE', #15891, #3203, #7940 ) ;
#17322=FACE_OUTER_BOUND ( 'NONE', #5551, .T. ) ;
#17326=CARTESIAN_POINT ( 'NONE',  ( 31.00000000000000000, 11.00000000000000000, 30.99999999999999289 ) ) ;
#17336=EDGE_CURVE ( 'NONE', #9984, #13589, #11430, .T. ) ;
#17345=CARTESIAN_POINT ( 'NONE',  ( 31.00000000000000000, 19.00000000000000000, -31.00000000000000355 ) ) ;
#17348=FACE_OUTER_BOUND ( 'NONE', #14878, .T. ) ;
#17363=ORIENTED_EDGE ( 'NONE', *, *, #399, .F. ) ;
#17383=DIRECTION ( 'NONE',  ( -1.000000000000000000, 0.000000000000000000, 0.000000000000000000 ) ) ;
#17385=ORIENTED_EDGE ( 'NONE', *, *, #9257, .F. ) ;
#17393=DIRECTION ( 'NONE',  ( 0.000000000000000000, 1.000000000000000000, 0.000000000000000000 ) ) ;
#17404=ORIENTED_EDGE ( 'NONE', *, *, #17667, .T. ) ;
#17408=DIRECTION ( 'NONE',  ( 0.000000000000000000, 0.000000000000000000, -1.000000000000000000 ) ) ;
#17409=CARTESIAN_POINT ( 'NONE',  ( -40.00000000000000000, 19.00000000000000000, 25.99999999999999645 ) ) ;
#17411=EDGE_CURVE ( 'NONE', #9677, #12613, #10565, .T. ) ;
#17419=ADVANCED_FACE ( 'NONE', ( #17805 ), #7109, .F. ) ;
#17441=EDGE_CURVE ( 'NONE', #17030, #3979, #10926, .T. ) ;
#17454=DIRECTION ( 'NONE',  ( -0.000000000000000000, -1.000000000000000000, -0.000000000000000000 ) ) ;
#17486=DIRECTION ( 'NONE',  ( -0.000000000000000000, -1.000000000000000000, -0.000000000000000000 ) ) ;
#17494=VECTOR ( 'NONE', #2077, 1000.000000000000000 ) ;
#17508=PLANE ( 'NONE',  #18560 ) ;
#17522=VERTEX_POINT ( 'NONE', #2747 ) ;
#17523=AXIS2_PLACEMENT_3D ( 'NONE', #17073, #3260, #17166 ) ;
#17527=DIRECTION ( 'NONE',  ( 0.000000000000000000, 0.000000000000000000, 1.000000000000000000 ) ) ;
#17545=DIRECTION ( 'NONE',  ( -0.000000000000000000, -1.000000000000000000, -0.000000000000000000 ) ) ;
#17586=ORIENTED_EDGE ( 'NONE', *, *, #6131, .F. ) ;
#17592=VECTOR ( 'NONE', #9104, 1000.000000000000000 ) ;
#17596=EDGE_LOOP ( 'NONE', ( #7505, #459 ) ) ;
#17597=EDGE_CURVE ( 'NONE', #19312, #10280, #1686, .T. ) ;
#17615=EDGE_LOOP ( 'NONE', ( #2713, #3294, #8036, #1084 ) ) ;
#17617=ORIENTED_EDGE ( 'NONE', *, *, #19444, .T. ) ;
#17630=EDGE_CURVE ( 'NONE', #18105, #7143, #4344, .T. ) ;
#17643=ORIENTED_EDGE ( 'NONE', *, *, #19714, .T. ) ;
#17646=ORIENTED_EDGE ( 'NONE', *, *, #2947, .T. ) ;
#17665=EDGE_LOOP ( 'NONE', ( #16323, #12235, #13560, #3584 ) ) ;
#17667=EDGE_CURVE ( 'NONE', #298, #18105, #3878, .T. ) ;
#17678=DIRECTION ( 'NONE',  ( -0.000000000000000000, -1.000000000000000000, -0.000000000000000000 ) ) ;
#17686=EDGE_CURVE ( 'NONE', #5571, #10263, #16171, .T. ) ;
#17704=CARTESIAN_POINT ( 'NONE',  ( 0.000000000000000000, 0.000000000000000000, 0.000000000000000000 ) ) ;
#17705=LINE ( 'NONE', #11521, #15655 ) ;
#17706=DIRECTION ( 'NONE',  ( -0.000000000000000000, -1.000000000000000000, -0.000000000000000000 ) ) ;
#17714=ORIENTED_EDGE ( 'NONE', *, *, #2312, .T. ) ;
#17715=ORIENTED_EDGE ( 'NONE', *, *, #4845, .F. ) ;
#17718=CARTESIAN_POINT ( 'NONE',  ( 4.286263797015737285E-15, -3.000000000000000000, -35.00000000000000711 ) ) ;
#17749=CIRCLE ( 'NONE', #12817, 3.299999999999997158 ) ;
#17762=VERTEX_POINT ( 'NONE', #16855 ) ;
#17766=LINE ( 'NONE', #17970, #18867 ) ;
#17770=VECTOR ( 'NONE', #12341, 1000.000000000000000 ) ;
#17771=CARTESIAN_POINT ( 'NONE',  ( 40.00000000000000711, 11.00000000000000000, -26.00000000000000355 ) ) ;
#17787=ORIENTED_EDGE ( 'NONE', *, *, #9777, .T. ) ;
#17796=CARTESIAN_POINT ( 'NONE',  ( -34.99999999999996447, 8.000000000000000000, 40.00000000000000711 ) ) ;
#17798=DIRECTION ( 'NONE',  ( -0.000000000000000000, -1.000000000000000000, -0.000000000000000000 ) ) ;
#17800=DIRECTION ( 'NONE',  ( -0.000000000000000000, -1.000000000000000000, -0.000000000000000000 ) ) ;
#17805=FACE_OUTER_BOUND ( 'NONE', #17615, .T. ) ;
#17842=DIRECTION ( 'NONE',  ( -0.000000000000000000, -0.000000000000000000, 1.000000000000000000 ) ) ;
#17864=PRODUCT_DEFINITION_FORMATION_WITH_SPECIFIED_SOURCE ( 'ANY', '', #7941, .NOT_KNOWN. ) ;
#17869=FILL_AREA_STYLE ('',( #1984 ) ) ;
#17902=( NAMED_UNIT ( * ) SI_UNIT ( $, .STERADIAN. ) SOLID_ANGLE_UNIT ( ) );
#17925=VECTOR ( 'NONE', #19774, 1000.000000000000000 ) ;
#17958=ORIENTED_EDGE ( 'NONE', *, *, #8890, .T. ) ;
#17967=EDGE_CURVE ( 'NONE', #11244, #3628, #1874, .T. ) ;
#17970=CARTESIAN_POINT ( 'NONE',  ( 31.00000000000003553, 11.00000000000000000, -26.00000000000000355 ) ) ;
#17971=FACE_OUTER_BOUND ( 'NONE', #3153, .T. ) ;
#17986=EDGE_CURVE ( 'NONE', #9564, #19183, #8089, .T. ) ;
#17989=VERTEX_POINT ( 'NONE', #11261 ) ;
#17993=LINE ( 'NONE', #13385, #7804 ) ;
#18007=VERTEX_POINT ( 'NONE', #6650 ) ;
#18020=LINE ( 'NONE', #10880, #12687 ) ;
#18040=EDGE_CURVE ( 'NONE', #14347, #9830, #8953, .T. ) ;
#18062=DIRECTION ( 'NONE',  ( 0.000000000000000000, 0.000000000000000000, -1.000000000000000000 ) ) ;
#18063=ADVANCED_FACE ( 'NONE', ( #19727 ), #2743, .T. ) ;
#18066=ORIENTED_EDGE ( 'NONE', *, *, #15477, .F. ) ;
#18095=LINE ( 'NONE', #1177, #2 ) ;
#18105=VERTEX_POINT ( 'NONE', #13682 ) ;
#18112=DIRECTION ( 'NONE',  ( 0.000000000000000000, 0.000000000000000000, 1.000000000000000000 ) ) ;
#18118=FACE_OUTER_BOUND ( 'NONE', #10355, .T. ) ;
#18139=PLANE ( 'NONE',  #413 ) ;
#18145=LINE ( 'NONE', #2593, #7382 ) ;
#18167=VECTOR ( 'NONE', #19321, 1000.000000000000000 ) ;
#18168=CARTESIAN_POINT ( 'NONE',  ( -31.81980515339462912, 11.00000000000000000, -31.81980515339465043 ) ) ;
#18195=AXIS2_PLACEMENT_3D ( 'NONE', #18825, #17393, #14310 ) ;
#18203=LINE ( 'NONE', #8932, #13176 ) ;
#18205=ORIENTED_EDGE ( 'NONE', *, *, #12904, .F. ) ;
#18224=DIRECTION ( 'NONE',  ( 0.000000000000000000, 0.000000000000000000, 1.000000000000000000 ) ) ;
#18230=AXIS2_PLACEMENT_3D ( 'NONE', #741, #1979, #7062 ) ;
#18235=VERTEX_POINT ( 'NONE', #19413 ) ;
#18243=CARTESIAN_POINT ( 'NONE',  ( -35.00000000000000000, 19.00000000000000000, -21.00000000000000000 ) ) ;
#18244=AXIS2_PLACEMENT_3D ( 'NONE', #10906, #12454, #4618 ) ;
#18245=CARTESIAN_POINT ( 'NONE',  ( -31.81980515339462912, 0.000000000000000000, 31.81980515339465043 ) ) ;
#18257=DIRECTION ( 'NONE',  ( 0.000000000000000000, 0.000000000000000000, -1.000000000000000000 ) ) ;
#18261=LINE ( 'NONE', #2385, #18558 ) ;
#18294=CARTESIAN_POINT ( 'NONE',  ( -35.00000000000000000, 19.00000000000000000, 20.99999999999999289 ) ) ;
#18299=EDGE_CURVE ( 'NONE', #14156, #3610, #13161, .T. ) ;
#18304=EDGE_CURVE ( 'NONE', #8469, #4676, #6564, .T. ) ;
#18321=DIRECTION ( 'NONE',  ( 0.000000000000000000, 1.000000000000000000, -0.000000000000000000 ) ) ;
#18328=LINE ( 'NONE', #13417, #5606 ) ;
#18330=CARTESIAN_POINT ( 'NONE',  ( 0.000000000000000000, -3.000000000000000000, 0.000000000000000000 ) ) ;
#18332=LINE ( 'NONE', #10414, #5310 ) ;
#18355=EDGE_CURVE ( 'NONE', #11036, #975, #18852, .T. ) ;
#18357=VECTOR ( 'NONE', #15430, 1000.000000000000000 ) ;
#18365=ADVANCED_FACE ( 'NONE', ( #1430 ), #20201, .F. ) ;
#18380=CIRCLE ( 'NONE', #8199, 3.300000000000004263 ) ;
#18395=LINE ( 'NONE', #877, #19872 ) ;
#18397=DIRECTION ( 'NONE',  ( -1.000000000000000000, -0.000000000000000000, -0.000000000000000000 ) ) ;
#18413=DIRECTION ( 'NONE',  ( -0.000000000000000000, -1.000000000000000000, -0.000000000000000000 ) ) ;
#18424=AXIS2_PLACEMENT_3D ( 'NONE', #19552, #18321, #602 ) ;
#18441=CARTESIAN_POINT ( 'NONE',  ( 34.99999999999997868, 11.00000000000000000, -40.00000000000000711 ) ) ;
#18451=VERTEX_POINT ( 'NONE', #15025 ) ;
#18453=LINE ( 'NONE', #20205, #11659 ) ;
#18457=ORIENTED_EDGE ( 'NONE', *, *, #5096, .F. ) ;
#18469=CARTESIAN_POINT ( 'NONE',  ( -35.00000000000000000, 19.00000000000000000, 20.99999999999999289 ) ) ;
#18483=ORIENTED_EDGE ( 'NONE', *, *, #17411, .F. ) ;
#18531=AXIS2_PLACEMENT_3D ( 'NONE', #6641, #11858, #18224 ) ;
#18558=VECTOR ( 'NONE', #846, 1000.000000000000000 ) ;
#18560=AXIS2_PLACEMENT_3D ( 'NONE', #17326, #20199, #15486 ) ;
#18561=EDGE_CURVE ( 'NONE', #15692, #18007, #12440, .T. ) ;
#18571=DIRECTION ( 'NONE',  ( -1.000000000000000000, -0.000000000000000000, -0.000000000000000000 ) ) ;
#18573=CARTESIAN_POINT ( 'NONE',  ( 31.00000000000003553, 8.000000000000000000, 20.99999999999999289 ) ) ;
#18574=ORIENTED_EDGE ( 'NONE', *, *, #6231, .F. ) ;
#18581=FACE_OUTER_BOUND ( 'NONE', #2854, .T. ) ;
#18598=VECTOR ( 'NONE', #3042, 1000.000000000000000 ) ;
#18606=PLANE ( 'NONE',  #464 ) ;
#18607=VECTOR ( 'NONE', #13670, 1000.000000000000000 ) ;
#18618=LINE ( 'NONE', #17277, #18598 ) ;
#18624=ORIENTED_EDGE ( 'NONE', *, *, #19057, .F. ) ;
#18626=ORIENTED_EDGE ( 'NONE', *, *, #18956, .F. ) ;
#18635=ORIENTED_EDGE ( 'NONE', *, *, #19281, .F. ) ;
#18641=FACE_OUTER_BOUND ( 'NONE', #4404, .T. ) ;
#18653=ORIENTED_EDGE ( 'NONE', *, *, #3211, .F. ) ;
#18663=LINE ( 'NONE', #14510, #15119 ) ;
#18702=CARTESIAN_POINT ( 'NONE',  ( -31.81980515339462912, 8.000000000000000000, 31.81980515339465043 ) ) ;
#18714=PLANE ( 'NONE',  #14130 ) ;
#18717=EDGE_LOOP ( 'NONE', ( #795, #19243 ) ) ;
#18719=CARTESIAN_POINT ( 'NONE',  ( 40.00000000000000711, 11.00000000000000000, 34.99999999999997868 ) ) ;
#18727=ADVANCED_FACE ( 'NONE', ( #3363 ), #11092, .F. ) ;
#18754=CIRCLE ( 'NONE', #11862, 4.999999999999997335 ) ;
#18769=ORIENTED_EDGE ( 'NONE', *, *, #7097, .F. ) ;
#18771=DIRECTION ( 'NONE',  ( -0.000000000000000000, -1.000000000000000000, -0.000000000000000000 ) ) ;
#18776=EDGE_CURVE ( 'NONE', #8466, #13536, #11286, .T. ) ;
#18790=EDGE_LOOP ( 'NONE', ( #485, #15469, #16857, #980 ) ) ;
#18794=DIRECTION ( 'NONE',  ( 0.000000000000000000, 0.000000000000000000, -1.000000000000000000 ) ) ;
#18825=CARTESIAN_POINT ( 'NONE',  ( -31.00000000000000000, 11.00000000000000000, -31.00000000000000000 ) ) ;
#18841=DIRECTION ( 'NONE',  ( 0.000000000000000000, 0.000000000000000000, 1.000000000000000000 ) ) ;
#18852=LINE ( 'NONE', #20303, #420 ) ;
#18860=ORIENTED_EDGE ( 'NONE', *, *, #5878, .T. ) ;
#18867=VECTOR ( 'NONE', #16538, 1000.000000000000000 ) ;
#18877=CYLINDRICAL_SURFACE ( 'NONE', #1446, 9.999999999999998224 ) ;
#18882=CIRCLE ( 'NONE', #9007, 4.999999999999997335 ) ;
#18914=CARTESIAN_POINT ( 'NONE',  ( -31.81980515339462912, 8.000000000000000000, 31.81980515339465043 ) ) ;
#18919=STYLED_ITEM ( 'NONE', ( #16359 ), #1227 ) ;
#18939=ADVANCED_FACE ( 'NONE', ( #13750, #13655 ), #5918, .F. ) ;
#18951=AXIS2_PLACEMENT_3D ( 'NONE', #12576, #1302, #18841 ) ;
#18956=EDGE_CURVE ( 'NONE', #13165, #8469, #15263, .T. ) ;
#18963=CARTESIAN_POINT ( 'NONE',  ( -34.99999999999996447, 8.000000000000000000, -40.00000000000000711 ) ) ;
#18969=DIRECTION ( 'NONE',  ( 0.000000000000000000, 0.000000000000000000, 1.000000000000000000 ) ) ;
#18971=LINE ( 'NONE', #14446, #4458 ) ;
#18983=ORIENTED_EDGE ( 'NONE', *, *, #20178, .T. ) ;
#18985=ORIENTED_EDGE ( 'NONE', *, *, #15171, .F. ) ;
#18989=EDGE_LOOP ( 'NONE', ( #16954, #5143, #4400, #2923 ) ) ;
#18993=FACE_OUTER_BOUND ( 'NONE', #18790, .T. ) ;
#19001=ORIENTED_EDGE ( 'NONE', *, *, #10506, .F. ) ;
#19026=DIRECTION ( 'NONE',  ( 0.000000000000000000, 0.000000000000000000, 1.000000000000000000 ) ) ;
#19044=DIRECTION ( 'NONE',  ( -0.000000000000000000, -1.000000000000000000, -0.000000000000000000 ) ) ;
#19057=EDGE_CURVE ( 'NONE', #16598, #11036, #6233, .T. ) ;
#19073=CARTESIAN_POINT ( 'NONE',  ( 31.00000000000006750, 19.00000000000000000, -21.00000000000000355 ) ) ;
#19092=ADVANCED_FACE ( 'NONE', ( #20235 ), #7672, .F. ) ;
#19172=CARTESIAN_POINT ( 'NONE',  ( 31.00000000000000000, 19.00000000000000000, -21.00000000000000355 ) ) ;
#19177=ADVANCED_FACE ( 'NONE', ( #14869 ), #14764, .F. ) ;
#19183=VERTEX_POINT ( 'NONE', #10133 ) ;
#19214=CARTESIAN_POINT ( 'NONE',  ( -35.00000000000000000, 8.000000000000000000, -21.00000000000000000 ) ) ;
#19215=AXIS2_PLACEMENT_3D ( 'NONE', #8190, #19486, #9829 ) ;
#19223=EDGE_CURVE ( 'NONE', #6022, #183, #18261, .T. ) ;
#19225=VECTOR ( 'NONE', #535, 1000.000000000000000 ) ;
#19239=ORIENTED_EDGE ( 'NONE', *, *, #14754, .F. ) ;
#19243=ORIENTED_EDGE ( 'NONE', *, *, #17597, .T. ) ;
#19281=EDGE_CURVE ( 'NONE', #16049, #12403, #18145, .T. ) ;
#19283=DIRECTION ( 'NONE',  ( -0.000000000000000000, -1.000000000000000000, -0.000000000000000000 ) ) ;
#19291=DIRECTION ( 'NONE',  ( -1.000000000000000000, 0.000000000000000000, 0.000000000000000000 ) ) ;
#19293=ORIENTED_EDGE ( 'NONE', *, *, #10398, .T. ) ;
#19298=CARTESIAN_POINT ( 'NONE',  ( -31.81980515339462912, 11.00000000000000000, 35.11980515339465825 ) ) ;
#19302=DIRECTION ( 'NONE',  ( 0.000000000000000000, 0.000000000000000000, 1.000000000000000000 ) ) ;
#19312=VERTEX_POINT ( 'NONE', #12803 ) ;
#19319=FACE_BOUND ( 'NONE', #2822, .T. ) ;
#19321=DIRECTION ( 'NONE',  ( -0.000000000000000000, -1.000000000000000000, -0.000000000000000000 ) ) ;
#19334=CARTESIAN_POINT ( 'NONE',  ( -34.99999999999996447, 0.000000000000000000, 40.00000000000000711 ) ) ;
#19344=DIRECTION ( 'NONE',  ( 0.000000000000000000, 1.000000000000000000, 0.000000000000000000 ) ) ;
#19377=FACE_OUTER_BOUND ( 'NONE', #551, .T. ) ;
#19380=CARTESIAN_POINT ( 'NONE',  ( -20.99999999999999645, 8.000000000000000000, -31.00000000000003908 ) ) ;
#19387=DIRECTION ( 'NONE',  ( -0.000000000000000000, -1.000000000000000000, -0.000000000000000000 ) ) ;
#19409=CARTESIAN_POINT ( 'NONE',  ( 21.00000000000000000, 19.00000000000000000, 31.00000000000006395 ) ) ;
#19413=CARTESIAN_POINT ( 'NONE',  ( -31.81980515339462912, 11.00000000000000000, 28.51980515339464617 ) ) ;
#19417=ORIENTED_EDGE ( 'NONE', *, *, #17967, .F. ) ;
#19419=AXIS2_PLACEMENT_3D ( 'NONE', #5880, #1100, #2968 ) ;
#19422=DIRECTION ( 'NONE',  ( -0.000000000000000000, -1.000000000000000000, -0.000000000000000000 ) ) ;
#19423=CARTESIAN_POINT ( 'NONE',  ( 21.00000000000000000, 8.000000000000000000, -31.00000000000003908 ) ) ;
#19429=DIRECTION ( 'NONE',  ( 1.000000000000000000, 0.000000000000000000, -0.000000000000000000 ) ) ;
#19441=LINE ( 'NONE', #5347, #6250 ) ;
#19442=EDGE_LOOP ( 'NONE', ( #19638, #19821, #3018, #7032 ) ) ;
#19444=EDGE_CURVE ( 'NONE', #19815, #14619, #8260, .T. ) ;
#19472=ORIENTED_EDGE ( 'NONE', *, *, #5322, .F. ) ;
#19476=EDGE_CURVE ( 'NONE', #19183, #298, #5181, .T. ) ;
#19480=DIRECTION ( 'NONE',  ( -0.000000000000000000, -1.000000000000000000, -0.000000000000000000 ) ) ;
#19486=DIRECTION ( 'NONE',  ( -0.000000000000000000, -1.000000000000000000, -0.000000000000000000 ) ) ;
#19491=CARTESIAN_POINT ( 'NONE',  ( -31.81980515339462912, 0.000000000000000000, -31.81980515339465043 ) ) ;
#19503=CARTESIAN_POINT ( 'NONE',  ( -31.00000000000000000, 19.00000000000000000, -31.00000000000000000 ) ) ;
#19515=ORIENTED_EDGE ( 'NONE', *, *, #1070, .F. ) ;
#19525=CARTESIAN_POINT ( 'NONE',  ( 21.00000000000000000, 19.00000000000000000, -35.00000000000000711 ) ) ;
#19533=FACE_BOUND ( 'NONE', #18717, .T. ) ;
#19541=UNCERTAINTY_MEASURE_WITH_UNIT (LENGTH_MEASURE( 1.000000000000000082E-05 ), #5342, 'distance_accuracy_value', 'NONE');
#19542=VECTOR ( 'NONE', #7555, 1000.000000000000000 ) ;
#19549=CARTESIAN_POINT ( 'NONE',  ( 26.00000000000000355, 19.00000000000000000, -31.00000000000004263 ) ) ;
#19552=CARTESIAN_POINT ( 'NONE',  ( -34.99999999999999289, 0.000000000000000000, -35.00000000000000711 ) ) ;
#19556=EDGE_CURVE ( 'NONE', #11244, #1495, #1435, .T. ) ;
#19560=LINE ( 'NONE', #810, #11032 ) ;
#19585=CARTESIAN_POINT ( 'NONE',  ( 26.00000000000000000, 19.00000000000000000, 31.00000000000003197 ) ) ;
#19590=VERTEX_POINT ( 'NONE', #5566 ) ;
#19596=ORIENTED_EDGE ( 'NONE', *, *, #9808, .T. ) ;
#19604=ORIENTED_EDGE ( 'NONE', *, *, #19678, .T. ) ;
#19623=CARTESIAN_POINT ( 'NONE',  ( -40.00000000000000000, 19.00000000000000000, -26.00000000000000355 ) ) ;
#19638=ORIENTED_EDGE ( 'NONE', *, *, #18561, .T. ) ;
#19646=FACE_OUTER_BOUND ( 'NONE', #11198, .T. ) ;
#19661=EDGE_LOOP ( 'NONE', ( #3005, #14990, #19604, #6817 ) ) ;
#19671=DIRECTION ( 'NONE',  ( 0.000000000000000000, 1.000000000000000000, 0.000000000000000000 ) ) ;
#19674=FACE_BOUND ( 'NONE', #13265, .T. ) ;
#19678=EDGE_CURVE ( 'NONE', #12591, #13473, #14491, .T. ) ;
#19710=ORIENTED_EDGE ( 'NONE', *, *, #19223, .T. ) ;
#19714=EDGE_CURVE ( 'NONE', #3873, #1902, #8556, .T. ) ;
#19716=EDGE_LOOP ( 'NONE', ( #10446, #14679, #13852, #12852 ) ) ;
#19727=FACE_OUTER_BOUND ( 'NONE', #16270, .T. ) ;
#19730=LINE ( 'NONE', #1172, #1469 ) ;
#19736=AXIS2_PLACEMENT_3D ( 'NONE', #4530, #12949, #6189 ) ;
#19741=LINE ( 'NONE', #4001, #13023 ) ;
#19758=DIRECTION ( 'NONE',  ( -0.000000000000000000, -0.000000000000000000, 1.000000000000000000 ) ) ;
#19762=EDGE_CURVE ( 'NONE', #15692, #16481, #9198, .T. ) ;
#19774=DIRECTION ( 'NONE',  ( -0.000000000000000000, -1.000000000000000000, -0.000000000000000000 ) ) ;
#19780=DIRECTION ( 'NONE',  ( 0.000000000000000000, -0.000000000000000000, 1.000000000000000000 ) ) ;
#19782=FACE_OUTER_BOUND ( 'NONE', #17665, .T. ) ;
#19791=EDGE_CURVE ( 'NONE', #4994, #15939, #14670, .T. ) ;
#19803=CARTESIAN_POINT ( 'NONE',  ( -34.99999999999999289, 11.00000000000000000, 40.00000000000000711 ) ) ;
#19815=VERTEX_POINT ( 'NONE', #19298 ) ;
#19821=ORIENTED_EDGE ( 'NONE', *, *, #10239, .F. ) ;
#19826=ORIENTED_EDGE ( 'NONE', *, *, #10065, .T. ) ;
#19831=ADVANCED_FACE ( 'NONE', ( #2267 ), #16342, .F. ) ;
#19839=PLANE ( 'NONE',  #12940 ) ;
#19855=CYLINDRICAL_SURFACE ( 'NONE', #11971, 3.299999999999997158 ) ;
#19872=VECTOR ( 'NONE', #9030, 1000.000000000000000 ) ;
#19886=DIRECTION ( 'NONE',  ( 1.000000000000000000, 0.000000000000000000, -0.000000000000000000 ) ) ;
#19904=CARTESIAN_POINT ( 'NONE',  ( 35.00000000000000711, 19.00000000000000000, -21.00000000000000355 ) ) ;
#19905=DIRECTION ( 'NONE',  ( 0.000000000000000000, 0.000000000000000000, 1.000000000000000000 ) ) ;
#19957=CARTESIAN_POINT ( 'NONE',  ( -31.81980515339462912, 8.000000000000000000, -31.81980515339465043 ) ) ;
#19965=DIRECTION ( 'NONE',  ( 0.000000000000000000, 0.000000000000000000, -1.000000000000000000 ) ) ;
#19967=LINE ( 'NONE', #1195, #10561 ) ;
#19973=ORIENTED_EDGE ( 'NONE', *, *, #5231, .F. ) ;
#19983=CIRCLE ( 'NONE', #2557, 18.50000000000000000 ) ;
#20006=DIRECTION ( 'NONE',  ( 0.000000000000000000, 0.000000000000000000, -1.000000000000000000 ) ) ;
#20049=LINE ( 'NONE', #13998, #7138 ) ;
#20053=FACE_OUTER_BOUND ( 'NONE', #14124, .T. ) ;
#20055=VERTEX_POINT ( 'NONE', #13416 ) ;
#20067=AXIS2_PLACEMENT_3D ( 'NONE', #10211, #7146, #4340 ) ;
#20075=EDGE_CURVE ( 'NONE', #16481, #9564, #10640, .T. ) ;
#20107=LINE ( 'NONE', #7654, #15980 ) ;
#20110=ORIENTED_EDGE ( 'NONE', *, *, #14282, .F. ) ;
#20113=LINE ( 'NONE', #7360, #17258 ) ;
#20156=EDGE_CURVE ( 'NONE', #17182, #14898, #9320, .T. ) ;
#20178=EDGE_CURVE ( 'NONE', #16867, #8912, #13893, .T. ) ;
#20181=EDGE_LOOP ( 'NONE', ( #14066, #18635, #1313, #855 ) ) ;
#20199=DIRECTION ( 'NONE',  ( 0.000000000000000000, 1.000000000000000000, 0.000000000000000000 ) ) ;
#20201=PLANE ( 'NONE',  #4711 ) ;
#20205=CARTESIAN_POINT ( 'NONE',  ( -26.00000000000000000, 19.00000000000000000, 40.00000000000001421 ) ) ;
#20206=CIRCLE ( 'NONE', #12311, 4.999999999999997335 ) ;
#20219=VECTOR ( 'NONE', #19283, 1000.000000000000000 ) ;
#20228=DIRECTION ( 'NONE',  ( -0.000000000000000000, -1.000000000000000000, -0.000000000000000000 ) ) ;
#20229=CARTESIAN_POINT ( 'NONE',  ( -31.00000000000006395, 19.00000000000000000, 20.99999999999998934 ) ) ;
#20235=FACE_OUTER_BOUND ( 'NONE', #14958, .T. ) ;
#20242=VECTOR ( 'NONE', #56, 1000.000000000000000 ) ;
#20253=CARTESIAN_POINT ( 'NONE',  ( 31.00000000000006750, 8.000000000000000000, -21.00000000000000355 ) ) ;
#20256=DIRECTION ( 'NONE',  ( -0.000000000000000000, -1.000000000000000000, -0.000000000000000000 ) ) ;
#20267=ADVANCED_FACE ( 'NONE', ( #18641 ), #2561, .F. ) ;
#20284=EDGE_LOOP ( 'NONE', ( #6886, #17715 ) ) ;
#20294=EDGE_CURVE ( 'NONE', #6864, #20055, #1064, .T. ) ;
#20301=DIRECTION ( 'NONE',  ( 0.000000000000000000, 0.000000000000000000, 1.000000000000000000 ) ) ;
#20303=CARTESIAN_POINT ( 'NONE',  ( -20.99999999999999645, 8.000000000000000000, 35.00000000000001421 ) ) ;
#20333=ORIENTED_EDGE ( 'NONE', *, *, #12282, .T. ) ;
#20338=ORIENTED_EDGE ( 'NONE', *, *, #20294, .T. ) ;
#20345=DIRECTION ( 'NONE',  ( 0.000000000000000000, 0.000000000000000000, -1.000000000000000000 ) ) ;
#20360=FACE_OUTER_BOUND ( 'NONE', #8844, .T. ) ;
ENDSEC;
END-ISO-10303-21;
